ISO-10303-21;
HEADER;
FILE_DESCRIPTION (('STEP AP214'),
    '1' );
FILE_NAME ('Lower cage plate.step',
    '2026-10-12T23:53:07',
    ( '' ),
    ( '' ),
    'SwSTEP 2.0',
    'SolidWorks 2024',
    '' );
FILE_SCHEMA (( 'AUTOMOTIVE_DESIGN' ));
ENDSEC;

DATA;
#5=EDGE_LOOP ( 'NONE', ( #28695, #28375, #39300, #8290 ) ) ;
#21=CYLINDRICAL_SURFACE ( 'NONE', #16555, 0.1000000000000000056 ) ;
#26=DIRECTION ( 'NONE',  ( 0.000000000000000000, 0.000000000000000000, 1.000000000000000000 ) ) ;
#37=DIRECTION ( 'NONE',  ( -6.162975822039154730E-33, 0.000000000000000000, -1.000000000000000000 ) ) ;
#57=EDGE_LOOP ( 'NONE', ( #4186, #2029, #37849, #1328 ) ) ;
#180=CARTESIAN_POINT ( 'NONE',  ( 0.03113248654051816583, -0.2276394436010286959, -0.1339480508475833498 ) ) ;
#190=CONICAL_SURFACE ( 'NONE', #23156, 0.4614999999999880864, 1.047197551196599408 ) ;
#199=VERTEX_POINT ( 'NONE', #1000 ) ;
#218=CARTESIAN_POINT ( 'NONE',  ( 0.05999999999999990757, 0.4357424459509064985, 0.2678820090948821342 ) ) ;
#225=AXIS2_PLACEMENT_3D ( 'NONE', #2754, #12223, #24786 ) ;
#251=ORIENTED_EDGE ( 'NONE', *, *, #36675, .F. ) ;
#292=ORIENTED_EDGE ( 'NONE', *, *, #19551, .T. ) ;
#307=VECTOR ( 'NONE', #3224, 39.37007874015748143 ) ;
#343=CIRCLE ( 'NONE', #37090, 0.1000000000000008521 ) ;
#400=CARTESIAN_POINT ( 'NONE',  ( 0.03113248654051816583, 0.5209315849442470725, 0.3202538583802974070 ) ) ;
#401=AXIS2_PLACEMENT_3D ( 'NONE', #26984, #15048, #39733 ) ;
#402=ORIENTED_EDGE ( 'NONE', *, *, #3753, .T. ) ;
#492=EDGE_CURVE ( 'NONE', #18074, #24668, #16830, .T. ) ;
#513=EDGE_LOOP ( 'NONE', ( #35888, #34743, #40576, #33330 ) ) ;
#542=DIRECTION ( 'NONE',  ( -6.162975822039154730E-33, 0.000000000000000000, -1.000000000000000000 ) ) ;
#553=VERTEX_POINT ( 'NONE', #13801 ) ;
#624=CARTESIAN_POINT ( 'NONE',  ( 0.05999999999999990757, 0.6304109427692223822, -0.1442409525262416947 ) ) ;
#639=CARTESIAN_POINT ( 'NONE',  ( 0.000000000000000000, 0.000000000000000000, 0.000000000000000000 ) ) ;
#660=CARTESIAN_POINT ( 'NONE',  ( 0.03113248654051816583, 0.000000000000000000, 0.000000000000000000 ) ) ;
#663=DIRECTION ( 'NONE',  ( -1.000000000000000000, -7.857794173099924470E-32, -8.628166150854818811E-32 ) ) ;
#701=DIRECTION ( 'NONE',  ( -9.860761315262649757E-32, -0.8518913899333641071, -0.5237184928541297468 ) ) ;
#740=VECTOR ( 'NONE', #38641, 39.37007874015748143 ) ;
#772=CONICAL_SURFACE ( 'NONE', #33580, 0.04999999999999994726, 1.047197551196598964 ) ;
#798=ORIENTED_EDGE ( 'NONE', *, *, #21242, .F. ) ;
#815=CARTESIAN_POINT ( 'NONE',  ( 0.05999999999999990757, 0.5878163732725504298, -0.1704268771689479434 ) ) ;
#847=ORIENTED_EDGE ( 'NONE', *, *, #8033, .T. ) ;
#859=DIRECTION ( 'NONE',  ( 0.000000000000000000, 0.000000000000000000, -1.000000000000000000 ) ) ;
#892=VERTEX_POINT ( 'NONE', #10676 ) ;
#909=DIRECTION ( 'NONE',  ( -4.930380657631323784E-32, -0.7472307839325098566, -0.6645646360916346307 ) ) ;
#1000=CARTESIAN_POINT ( 'NONE',  ( 0.05999999999999990757, 0.8066736284972624293, -0.2400112280131874720 ) ) ;
#1002=EDGE_LOOP ( 'NONE', ( #38695, #33633, #31555, #292 ) ) ;
#1007=ORIENTED_EDGE ( 'NONE', *, *, #36131, .T. ) ;
#1098=ORIENTED_EDGE ( 'NONE', *, *, #7725, .F. ) ;
#1107=FACE_OUTER_BOUND ( 'NONE', #32350, .T. ) ;
#1126=( CONVERSION_BASED_UNIT ( 'INCH', #10967 ) LENGTH_UNIT ( ) NAMED_UNIT ( #23398 ) );
#1162=VERTEX_POINT ( 'NONE', #11046 ) ;
#1163=ADVANCED_FACE ( 'NONE', ( #7927, #20504, #20717, #14322 ), #26881, .F. ) ;
#1197=VERTEX_POINT ( 'NONE', #24398 ) ;
#1241=ORIENTED_EDGE ( 'NONE', *, *, #13651, .T. ) ;
#1290=ORIENTED_EDGE ( 'NONE', *, *, #492, .F. ) ;
#1328=ORIENTED_EDGE ( 'NONE', *, *, #40432, .F. ) ;
#1348=DIRECTION ( 'NONE',  ( -1.000000000000000000, -6.779273404243070203E-32, -4.314083075427408311E-32 ) ) ;
#1350=DIRECTION ( 'NONE',  ( -1.000000000000000000, -6.779273404243070203E-32, -4.314083075427408311E-32 ) ) ;
#1378=DIRECTION ( 'NONE',  ( 4.930380657631319405E-32, 0.4913225862583635584, 0.8709776783778060416 ) ) ;
#1477=EDGE_CURVE ( 'NONE', #26774, #34185, #17752, .T. ) ;
#1486=VECTOR ( 'NONE', #8415, 39.37007874015748143 ) ;
#1503=DIRECTION ( 'NONE',  ( -0.4999999999999988343, -3.389636702121527438E-32, 0.8660254037844391517 ) ) ;
#1521=CONICAL_SURFACE ( 'NONE', #24503, 0.2000000000000000111, 1.047197551196598964 ) ;
#1571=AXIS2_PLACEMENT_3D ( 'NONE', #639, #13130, #37 ) ;
#1635=AXIS2_PLACEMENT_3D ( 'NONE', #14109, #1980, #14502 ) ;
#1684=ORIENTED_EDGE ( 'NONE', *, *, #33671, .F. ) ;
#1717=EDGE_CURVE ( 'NONE', #15843, #7929, #5984, .T. ) ;
#1782=CARTESIAN_POINT ( 'NONE',  ( 0.05999999999999990757, 0.000000000000000000, 0.06250000000000000000 ) ) ;
#1813=CYLINDRICAL_SURFACE ( 'NONE', #34915, 0.06250000000000000000 ) ;
#1950=EDGE_LOOP ( 'NONE', ( #15524, #18844, #37509, #37294, #24907, #13662, #26137, #12030, #33143, #33196, #16859 ) ) ;
#1951=ORIENTED_EDGE ( 'NONE', *, *, #22792, .F. ) ;
#1962=CARTESIAN_POINT ( 'NONE',  ( 0.03113248654051816583, 0.000000000000000000, 0.000000000000000000 ) ) ;
#1980=DIRECTION ( 'NONE',  ( 1.000000000000000000, 6.779273404243070203E-32, 4.314083075427408311E-32 ) ) ;
#1996=CARTESIAN_POINT ( 'NONE',  ( 0.03113248654051816583, 0.6410130462957083219, -0.4300623794142590661 ) ) ;
#2029=ORIENTED_EDGE ( 'NONE', *, *, #20334, .T. ) ;
#2149=CONICAL_SURFACE ( 'NONE', #31709, 0.2000000000000000111, 1.047197551196598964 ) ;
#2188=AXIS2_PLACEMENT_3D ( 'NONE', #6580, #28820, #6393 ) ;
#2211=VECTOR ( 'NONE', #12735, 39.37007874015748143 ) ;
#2233=VECTOR ( 'NONE', #30402, 39.37007874015748143 ) ;
#2266=VECTOR ( 'NONE', #8685, 39.37007874015748143 ) ;
#2273=DIRECTION ( 'NONE',  ( 0.000000000000000000, 0.000000000000000000, 1.000000000000000000 ) ) ;
#2327=PLANE ( 'NONE',  #19127 ) ;
#2350=ORIENTED_EDGE ( 'NONE', *, *, #29609, .T. ) ;
#2356=LINE ( 'NONE', #17972, #33054 ) ;
#2360=CARTESIAN_POINT ( 'NONE',  ( 2.696301922142129168E-33, 7.654042494670954463E-18, -0.06250000000000000000 ) ) ;
#2391=ADVANCED_FACE ( 'NONE', ( #38056 ), #9505, .F. ) ;
#2433=DIRECTION ( 'NONE',  ( -1.000000000000000000, -7.857794173099924470E-32, -8.628166150854818811E-32 ) ) ;
#2434=CARTESIAN_POINT ( 'NONE',  ( 0.05999999999999990757, 0.000000000000000000, 0.5614999999999926716 ) ) ;
#2466=DIRECTION ( 'NONE',  ( 1.000000000000000000, 6.779273404243070203E-32, 4.314083075427408311E-32 ) ) ;
#2484=CARTESIAN_POINT ( 'NONE',  ( 0.05999999999999990757, 0.5878163732725504298, -0.2704268771689488093 ) ) ;
#2562=DIRECTION ( 'NONE',  ( -0.4999999999999986677, 0.4254978411528150262, 0.7542887956043727860 ) ) ;
#2669=EDGE_LOOP ( 'NONE', ( #39297, #28607, #28151, #9412, #11173 ) ) ;
#2754=CARTESIAN_POINT ( 'NONE',  ( 0.05999999999999990757, 0.000000000000000000, 0.000000000000000000 ) ) ;
#2773=EDGE_LOOP ( 'NONE', ( #36991, #11699, #3234, #14701 ) ) ;
#2788=CARTESIAN_POINT ( 'NONE',  ( 0.05999999999999990757, 0.2217800815169825301, -0.07875759618522079619 ) ) ;
#2816=AXIS2_PLACEMENT_3D ( 'NONE', #30224, #5126, #9044 ) ;
#2826=DIRECTION ( 'NONE',  ( -1.000000000000000000, -7.857794173099924470E-32, -8.628166150854818811E-32 ) ) ;
#2836=ORIENTED_EDGE ( 'NONE', *, *, #37298, .F. ) ;
#2840=DIRECTION ( 'NONE',  ( -1.000000000000000000, -6.779273404243070203E-32, -4.314083075427408311E-32 ) ) ;
#2877=ORIENTED_EDGE ( 'NONE', *, *, #21233, .T. ) ;
#2893=ADVANCED_FACE ( 'NONE', ( #37349 ), #14945, .F. ) ;
#2912=CARTESIAN_POINT ( 'NONE',  ( 0.05999999999999990757, -0.03575622569115821658, -0.2978615321325044363 ) ) ;
#2930=LINE ( 'NONE', #18776, #12567 ) ;
#2948=CIRCLE ( 'NONE', #25961, 0.4614999999999880864 ) ;
#2961=DIRECTION ( 'NONE',  ( 0.000000000000000000, 0.000000000000000000, 1.000000000000000000 ) ) ;
#3007=UNCERTAINTY_MEASURE_WITH_UNIT (LENGTH_MEASURE( 1.000000000000000082E-05 ), #7004, 'distance_accuracy_value', 'NONE');
#3013=CARTESIAN_POINT ( 'NONE',  ( 0.05999999999999990757, 0.7171888913565960255, -0.2950238883388468514 ) ) ;
#3037=LINE ( 'NONE', #400, #20652 ) ;
#3043=CARTESIAN_POINT ( 'NONE',  ( 0.05999999999999990757, 0.6655791756086271160, -0.3865134954953681201 ) ) ;
#3045=EDGE_CURVE ( 'NONE', #14658, #25089, #29893, .T. ) ;
#3100=CARTESIAN_POINT ( 'NONE',  ( 0.05999999999999990757, 0.6730055122658872291, -0.1180550278835343775 ) ) ;
#3104=DIRECTION ( 'NONE',  ( 0.000000000000000000, 0.000000000000000000, -1.000000000000000000 ) ) ;
#3172=CYLINDRICAL_SURFACE ( 'NONE', #28912, 0.06249999999999997918 ) ;
#3207=EDGE_CURVE ( 'NONE', #29747, #30067, #12156, .T. ) ;
#3224=DIRECTION ( 'NONE',  ( -2.157041537713702240E-32, 0.8709776783778059306, -0.4913225862583635584 ) ) ;
#3234=ORIENTED_EDGE ( 'NONE', *, *, #29852, .F. ) ;
#3267=CARTESIAN_POINT ( 'NONE',  ( 0.05999999999999990757, -0.3458405862425447119, -0.2552451372150014719 ) ) ;
#3290=DIRECTION ( 'NONE',  ( -1.000000000000000000, -6.779273404243070203E-32, -4.314083075427408311E-32 ) ) ;
#3302=CONICAL_SURFACE ( 'NONE', #11179, 0.04999999999999994726, 1.047197551196598964 ) ;
#3316=ORIENTED_EDGE ( 'NONE', *, *, #9778, .T. ) ;
#3355=CARTESIAN_POINT ( 'NONE',  ( 0.05999999999999990757, 0.5386841146467193919, -0.2575246450067292248 ) ) ;
#3361=CIRCLE ( 'NONE', #36783, 0.6114999999999938263 ) ;
#3365=VERTEX_POINT ( 'NONE', #30530 ) ;
#3418=VECTOR ( 'NONE', #25725, 39.37007874015748143 ) ;
#3500=EDGE_CURVE ( 'NONE', #16124, #5597, #18085, .T. ) ;
#3515=DIRECTION ( 'NONE',  ( 0.000000000000000000, 0.000000000000000000, -1.000000000000000000 ) ) ;
#3527=DIRECTION ( 'NONE',  ( 1.000000000000000000, 6.779273404243070203E-32, 4.314083075427408311E-32 ) ) ;
#3567=DIRECTION ( 'NONE',  ( 1.000000000000000000, 6.779273404243070203E-32, 4.314083075427408311E-32 ) ) ;
#3627=DIRECTION ( 'NONE',  ( -0.4492559606623142687, 0.000000000000000000, -0.8934030903289852388 ) ) ;
#3643=CARTESIAN_POINT ( 'NONE',  ( 0.03113248654051816583, -3.491513147198973073E-33, 0.6114999999999938263 ) ) ;
#3678=PLANE ( 'NONE',  #35645 ) ;
#3693=CARTESIAN_POINT ( 'NONE',  ( 0.03113248654051816583, -0.4415087982045245996, -0.1343585914930099934 ) ) ;
#3698=CIRCLE ( 'NONE', #29984, 0.2000000000000000111 ) ;
#3708=LINE ( 'NONE', #3100, #13474 ) ;
#3714=CIRCLE ( 'NONE', #22784, 0.1000000000000000056 ) ;
#3738=AXIS2_PLACEMENT_3D ( 'NONE', #5563, #5964, #8861 ) ;
#3746=ORIENTED_EDGE ( 'NONE', *, *, #7412, .T. ) ;
#3752=DIRECTION ( 'NONE',  ( -1.000000000000000000, -7.857794173099924470E-32, -8.628166150854818811E-32 ) ) ;
#3753=EDGE_CURVE ( 'NONE', #29747, #38278, #5587, .T. ) ;
#3838=DIRECTION ( 'NONE',  ( 1.000000000000000000, 6.779273404243070203E-32, 4.314083075427408311E-32 ) ) ;
#3878=VERTEX_POINT ( 'NONE', #37820 ) ;
#3885=EDGE_CURVE ( 'NONE', #17043, #33631, #16018, .T. ) ;
#3892=DIRECTION ( 'NONE',  ( 2.157041537713702240E-32, -0.8709776783778059306, 0.4913225862583635584 ) ) ;
#3971=ORIENTED_EDGE ( 'NONE', *, *, #13695, .F. ) ;
#3983=ORIENTED_EDGE ( 'NONE', *, *, #20029, .F. ) ;
#4011=CARTESIAN_POINT ( 'NONE',  ( 0.05999999999999990757, 0.6730055122658872291, -0.1180550278835343775 ) ) ;
#4048=DIRECTION ( 'NONE',  ( -4.930380657631319405E-32, 0.5237184928541299689, -0.8518913899333637740 ) ) ;
#4131=ADVANCED_FACE ( 'NONE', ( #34476 ), #36744, .T. ) ;
#4144=ORIENTED_EDGE ( 'NONE', *, *, #15033, .T. ) ;
#4152=LINE ( 'NONE', #7041, #14895 ) ;
#4157=CIRCLE ( 'NONE', #11388, 0.1000000000000000194 ) ;
#4185=CIRCLE ( 'NONE', #38337, 0.1500000000000009936 ) ;
#4186=ORIENTED_EDGE ( 'NONE', *, *, #13651, .F. ) ;
#4239=DIRECTION ( 'NONE',  ( 0.000000000000000000, 0.000000000000000000, 1.000000000000000000 ) ) ;
#4244=DIRECTION ( 'NONE',  ( 1.000000000000000000, 6.779273404243070203E-32, 4.314083075427408311E-32 ) ) ;
#4332=EDGE_LOOP ( 'NONE', ( #12134, #19945, #33593, #38616 ) ) ;
#4363=EDGE_CURVE ( 'NONE', #35558, #9616, #28296, .T. ) ;
#4364=DIRECTION ( 'NONE',  ( -0.4999999999999988898, 0.5755298573121169214, -0.6471208413753147815 ) ) ;
#4379=ADVANCED_FACE ( 'NONE', ( #38569 ), #10390, .T. ) ;
#4386=VECTOR ( 'NONE', #2562, 39.37007874015747433 ) ;
#4390=ORIENTED_EDGE ( 'NONE', *, *, #22787, .T. ) ;
#4403=DIRECTION ( 'NONE',  ( 0.000000000000000000, 0.000000000000000000, -1.000000000000000000 ) ) ;
#4406=ORIENTED_EDGE ( 'NONE', *, *, #10456, .T. ) ;
#4440=EDGE_LOOP ( 'NONE', ( #20914, #35779, #3983, #39960 ) ) ;
#4461=CARTESIAN_POINT ( 'NONE',  ( 0.05999999999999990757, 0.07140090991423790612, -0.1319162994607513684 ) ) ;
#4490=CARTESIAN_POINT ( 'NONE',  ( 0.03113248654051816583, 0.000000000000000000, 0.000000000000000000 ) ) ;
#4527=ORIENTED_EDGE ( 'NONE', *, *, #21073, .F. ) ;
#4546=LINE ( 'NONE', #23313, #6056 ) ;
#4622=EDGE_CURVE ( 'NONE', #26774, #23647, #10583, .T. ) ;
#4639=LINE ( 'NONE', #39420, #22456 ) ;
#4659=DIRECTION ( 'NONE',  ( 1.000000000000000000, 6.779273404243070203E-32, 4.314083075427408311E-32 ) ) ;
#4711=CARTESIAN_POINT ( 'NONE',  ( 0.03113248654051816583, 0.000000000000000000, 0.000000000000000000 ) ) ;
#4776=ORIENTED_EDGE ( 'NONE', *, *, #5769, .F. ) ;
#4814=AXIS2_PLACEMENT_3D ( 'NONE', #11873, #39866, #9190 ) ;
#4830=CARTESIAN_POINT ( 'NONE',  ( 0.000000000000000000, 0.8492681979939306069, -0.2138253033704805295 ) ) ;
#5014=AXIS2_PLACEMENT_3D ( 'NONE', #17772, #5222, #11203 ) ;
#5024=DIRECTION ( 'NONE',  ( -1.000000000000000000, -6.779273404243070203E-32, -4.314083075427408311E-32 ) ) ;
#5063=DIRECTION ( 'NONE',  ( 1.000000000000000000, 6.779273404243070203E-32, 4.314083075427408311E-32 ) ) ;
#5096=EDGE_CURVE ( 'NONE', #29289, #14658, #23431, .T. ) ;
#5104=EDGE_CURVE ( 'NONE', #39766, #35558, #31887, .T. ) ;
#5105=EDGE_LOOP ( 'NONE', ( #22590, #19444, #18928, #28486 ) ) ;
#5116=CARTESIAN_POINT ( 'NONE',  ( 0.000000000000000000, 0.1969856463038233696, 0.03459270371430114843 ) ) ;
#5126=DIRECTION ( 'NONE',  ( -0.8660254037844394848, 0.3322823180458164272, -0.3736153919662538736 ) ) ;
#5222=DIRECTION ( 'NONE',  ( 1.000000000000000000, 6.779273404243070203E-32, 4.314083075427408311E-32 ) ) ;
#5223=FACE_OUTER_BOUND ( 'NONE', #2773, .T. ) ;
#5233=VERTEX_POINT ( 'NONE', #38656 ) ;
#5258=VECTOR ( 'NONE', #10278, 39.37007874015748143 ) ;
#5309=CARTESIAN_POINT ( 'NONE',  ( 0.05999999999999990757, 0.000000000000000000, 0.6114999999999938263 ) ) ;
#5329=EDGE_LOOP ( 'NONE', ( #7402, #38141, #34306, #29185, #28421, #4390, #29755, #11054, #5879, #32034 ) ) ;
#5363=EDGE_CURVE ( 'NONE', #7929, #15843, #20799, .T. ) ;
#5372=AXIS2_PLACEMENT_3D ( 'NONE', #15044, #24125, #5569 ) ;
#5377=LINE ( 'NONE', #18350, #8589 ) ;
#5407=CONICAL_SURFACE ( 'NONE', #19241, 0.1500000000000009936, 1.047197551196599630 ) ;
#5420=DIRECTION ( 'NONE',  ( 0.000000000000000000, 0.000000000000000000, 1.000000000000000000 ) ) ;
#5429=ORIENTED_EDGE ( 'NONE', *, *, #8033, .F. ) ;
#5436=EDGE_CURVE ( 'NONE', #5597, #24586, #3698, .T. ) ;
#5437=PLANE ( 'NONE',  #14047 ) ;
#5440=DIRECTION ( 'NONE',  ( 1.000000000000000000, 6.779273404243070203E-32, -6.162975822039154730E-33 ) ) ;
#5463=AXIS2_PLACEMENT_3D ( 'NONE', #11018, #23576, #17383 ) ;
#5486=ORIENTED_EDGE ( 'NONE', *, *, #31048, .T. ) ;
#5491=VECTOR ( 'NONE', #32208, 39.37007874015748854 ) ;
#5501=DIRECTION ( 'NONE',  ( 1.000000000000000000, 6.779273404243070203E-32, 4.314083075427408311E-32 ) ) ;
#5507=FACE_OUTER_BOUND ( 'NONE', #18611, .T. ) ;
#5512=ORIENTED_EDGE ( 'NONE', *, *, #14966, .F. ) ;
#5516=CIRCLE ( 'NONE', #34445, 0.1000000000000000194 ) ;
#5533=VECTOR ( 'NONE', #11107, 39.37007874015748143 ) ;
#5541=ORIENTED_EDGE ( 'NONE', *, *, #29814, .F. ) ;
#5563=CARTESIAN_POINT ( 'NONE',  ( 0.000000000000000000, -0.3458405862425447119, -0.1052451372150005060 ) ) ;
#5569=DIRECTION ( 'NONE',  ( 0.000000000000000000, 0.000000000000000000, -1.000000000000000000 ) ) ;
#5579=CARTESIAN_POINT ( 'NONE',  ( 0.05999999999999990757, 0.000000000000000000, 0.000000000000000000 ) ) ;
#5587=CIRCLE ( 'NONE', #401, 0.1000000000000000194 ) ;
#5597=VERTEX_POINT ( 'NONE', #36592 ) ;
#5608=ADVANCED_FACE ( 'NONE', ( #5507 ), #18165, .T. ) ;
#5688=EDGE_CURVE ( 'NONE', #34185, #38544, #40590, .T. ) ;
#5720=DIRECTION ( 'NONE',  ( -6.162975822039154730E-33, 0.000000000000000000, -1.000000000000000000 ) ) ;
#5727=EDGE_LOOP ( 'NONE', ( #36317, #31719, #31137, #19503 ) ) ;
#5734=CARTESIAN_POINT ( 'NONE',  ( 0.05999999999999990757, 0.7171888913565960255, -0.2950238883388468514 ) ) ;
#5746=PLANE ( 'NONE',  #2816 ) ;
#5769=EDGE_CURVE ( 'NONE', #23685, #26774, #36956, .T. ) ;
#5800=ORIENTED_EDGE ( 'NONE', *, *, #29614, .T. ) ;
#5833=ADVANCED_FACE ( 'NONE', ( #21738 ), #39196, .T. ) ;
#5842=CARTESIAN_POINT ( 'NONE',  ( 0.000000000000000000, -0.3852620677835773555, -0.4748740771268961103 ) ) ;
#5879=ORIENTED_EDGE ( 'NONE', *, *, #21242, .T. ) ;
#5880=DIRECTION ( 'NONE',  ( -1.000000000000000000, -6.779273404243070203E-32, -4.314083075427408311E-32 ) ) ;
#5906=DIRECTION ( 'NONE',  ( -6.162975822039151309E-33, 0.000000000000000000, -1.000000000000000000 ) ) ;
#5928=CARTESIAN_POINT ( 'NONE',  ( 0.03113248654051816583, 0.5878163732725504298, -0.2204268771689479045 ) ) ;
#5932=ADVANCED_FACE ( 'NONE', ( #24183 ), #11414, .F. ) ;
#5937=VERTEX_POINT ( 'NONE', #33835 ) ;
#5947=DIRECTION ( 'NONE',  ( 4.930380657631319405E-32, -0.5237184928541299689, 0.8518913899333638851 ) ) ;
#5964=DIRECTION ( 'NONE',  ( 1.000000000000000000, 6.779273404243070203E-32, 4.314083075427408311E-32 ) ) ;
#5984=CIRCLE ( 'NONE', #13879, 0.06250000000000001388 ) ;
#5986=ADVANCED_FACE ( 'NONE', ( #30935 ), #18385, .F. ) ;
#5989=ORIENTED_EDGE ( 'NONE', *, *, #11507, .F. ) ;
#5995=DIRECTION ( 'NONE',  ( 1.000000000000000000, 6.779273404243070203E-32, 4.314083075427408311E-32 ) ) ;
#6021=CIRCLE ( 'NONE', #32282, 0.2000000000000000111 ) ;
#6056=VECTOR ( 'NONE', #17111, 39.37007874015748143 ) ;
#6086=CARTESIAN_POINT ( 'NONE',  ( 0.000000000000000000, -0.2793841226333812489, -0.1799682156082512696 ) ) ;
#6091=VERTEX_POINT ( 'NONE', #25179 ) ;
#6121=EDGE_CURVE ( 'NONE', #15679, #29483, #8931, .T. ) ;
#6122=DIRECTION ( 'NONE',  ( 1.000000000000000000, 6.779273404243070203E-32, 4.314083075427408311E-32 ) ) ;
#6126=EDGE_CURVE ( 'NONE', #10562, #13712, #15914, .T. ) ;
#6131=CYLINDRICAL_SURFACE ( 'NONE', #20667, 0.04999999999999994726 ) ;
#6155=CARTESIAN_POINT ( 'NONE',  ( 0.03113248654051816583, -0.2793841226333812489, -0.1799682156082512696 ) ) ;
#6162=CYLINDRICAL_SURFACE ( 'NONE', #22545, 0.6114999999999938263 ) ;
#6178=LINE ( 'NONE', #27593, #17194 ) ;
#6203=CARTESIAN_POINT ( 'NONE',  ( 0.03113248654051816583, 0.1997995745459845707, -0.008951536808938304751 ) ) ;
#6207=DIRECTION ( 'NONE',  ( 0.000000000000000000, 0.000000000000000000, -1.000000000000000000 ) ) ;
#6236=AXIS2_PLACEMENT_3D ( 'NONE', #17613, #39823, #21108 ) ;
#6239=CYLINDRICAL_SURFACE ( 'NONE', #11466, 0.1000000000000000194 ) ;
#6253=DIRECTION ( 'NONE',  ( -1.000000000000000000, -6.779273404243070203E-32, -4.314083075427408311E-32 ) ) ;
#6264=FACE_OUTER_BOUND ( 'NONE', #17105, .T. ) ;
#6285=LINE ( 'NONE', #27696, #8052 ) ;
#6296=DIRECTION ( 'NONE',  ( 0.000000000000000000, 0.000000000000000000, 1.000000000000000000 ) ) ;
#6333=CARTESIAN_POINT ( 'NONE',  ( 0.05999999999999990757, 0.7171888913565960255, -0.3575238883388469069 ) ) ;
#6352=AXIS2_PLACEMENT_3D ( 'NONE', #21083, #27053, #5420 ) ;
#6375=DIRECTION ( 'NONE',  ( -1.000000000000000000, -7.857794173099924470E-32, -8.628166150854818811E-32 ) ) ;
#6388=LINE ( 'NONE', #28010, #25162 ) ;
#6393=DIRECTION ( 'NONE',  ( -6.162975822039154046E-33, 0.000000000000000000, -1.000000000000000000 ) ) ;
#6449=ORIENTED_EDGE ( 'NONE', *, *, #22513, .T. ) ;
#6492=PLANE ( 'NONE',  #12804 ) ;
#6498=EDGE_CURVE ( 'NONE', #24445, #27427, #17556, .T. ) ;
#6518=ORIENTED_EDGE ( 'NONE', *, *, #31034, .F. ) ;
#6532=DIRECTION ( 'NONE',  ( -1.000000000000000000, -7.857794173099924470E-32, -8.628166150854818811E-32 ) ) ;
#6553=AXIS2_PLACEMENT_3D ( 'NONE', #37137, #701, #19593 ) ;
#6580=CARTESIAN_POINT ( 'NONE',  ( 0.000000000000000000, 0.1428018198284763673, -0.2638325989215043466 ) ) ;
#6642=DIRECTION ( 'NONE',  ( -1.000000000000000000, -7.857794173099924470E-32, -8.628166150854818811E-32 ) ) ;
#6643=CIRCLE ( 'NONE', #24416, 0.5614999999999926716 ) ;
#6693=EDGE_CURVE ( 'NONE', #31055, #33631, #9009, .T. ) ;
#6754=ORIENTED_EDGE ( 'NONE', *, *, #1477, .F. ) ;
#6776=DIRECTION ( 'NONE',  ( -6.162975822039154730E-33, 0.000000000000000000, -1.000000000000000000 ) ) ;
#6799=DIRECTION ( 'NONE',  ( -6.162975822039154730E-33, 0.000000000000000000, -1.000000000000000000 ) ) ;
#6819=AXIS2_PLACEMENT_3D ( 'NONE', #34952, #29191, #19542 ) ;
#6832=DIRECTION ( 'NONE',  ( -6.162975822039154046E-33, 0.000000000000000000, -1.000000000000000000 ) ) ;
#6847=AXIS2_PLACEMENT_3D ( 'NONE', #34240, #5440, #14925 ) ;
#6858=EDGE_LOOP ( 'NONE', ( #5989, #20085, #30166, #15106 ) ) ;
#6861=CARTESIAN_POINT ( 'NONE',  ( 2.696301922142129510E-33, 0.7171888913565960255, -0.3575238883388469069 ) ) ;
#6871=VERTEX_POINT ( 'NONE', #8013 ) ;
#6878=AXIS2_PLACEMENT_3D ( 'NONE', #20397, #39501, #13802 ) ;
#6881=AXIS2_PLACEMENT_3D ( 'NONE', #10388, #1350, #26432 ) ;
#6912=CARTESIAN_POINT ( 'NONE',  ( 0.05999999999999990757, -2.357338251929976383E-33, 0.06250000000000000000 ) ) ;
#6975=AXIS2_PLACEMENT_3D ( 'NONE', #20769, #33292, #5906 ) ;
#7004=( CONVERSION_BASED_UNIT ( 'INCH', #18758 ) LENGTH_UNIT ( ) NAMED_UNIT ( #7294 ) );
#7013=CIRCLE ( 'NONE', #3738, 0.1000000000000000194 ) ;
#7041=CARTESIAN_POINT ( 'NONE',  ( 0.05999999999999990757, -0.4578766358967566452, -0.4053162176620347945 ) ) ;
#7147=LINE ( 'NONE', #7566, #16013 ) ;
#7164=EDGE_LOOP ( 'NONE', ( #34299, #19924 ) ) ;
#7172=DIRECTION ( 'NONE',  ( 1.000000000000000000, 6.779273404243070203E-32, 4.314083075427408311E-32 ) ) ;
#7191=ORIENTED_EDGE ( 'NONE', *, *, #7412, .F. ) ;
#7211=LINE ( 'NONE', #5842, #21280 ) ;
#7221=CARTESIAN_POINT ( 'NONE',  ( 0.05999999999999990757, 0.7171888913565960255, -0.3575238883388469069 ) ) ;
#7228=VECTOR ( 'NONE', #40521, 39.37007874015748143 ) ;
#7268=CARTESIAN_POINT ( 'NONE',  ( 0.05999999999999990757, 0.5878163732725504298, -0.1704268771689479434 ) ) ;
#7294=DIMENSIONAL_EXPONENTS ( 1.000000000000000000, 0.000000000000000000, 0.000000000000000000, 0.000000000000000000, 0.000000000000000000, 0.000000000000000000, 0.000000000000000000 ) ;
#7302=AXIS2_PLACEMENT_3D ( 'NONE', #22864, #7172, #859 ) ;
#7336=DIRECTION ( 'NONE',  ( -0.3961231183188304583, -5.551115123125781470E-17, -0.9181974053183585838 ) ) ;
#7339=AXIS2_PLACEMENT_3D ( 'NONE', #25772, #17103, #14010 ) ;
#7348=ORIENTED_EDGE ( 'NONE', *, *, #34780, .F. ) ;
#7352=FACE_OUTER_BOUND ( 'NONE', #4332, .T. ) ;
#7361=ADVANCED_FACE ( 'NONE', ( #34226 ), #3172, .F. ) ;
#7402=ORIENTED_EDGE ( 'NONE', *, *, #29814, .T. ) ;
#7412=EDGE_CURVE ( 'NONE', #34185, #20959, #3361, .T. ) ;
#7430=CARTESIAN_POINT ( 'NONE',  ( 0.03113248654051816583, 0.000000000000000000, 0.2000000000000000111 ) ) ;
#7444=DIRECTION ( 'NONE',  ( 1.000000000000000000, 6.779273404243070203E-32, 4.314083075427408311E-32 ) ) ;
#7509=DIRECTION ( 'NONE',  ( 0.000000000000000000, 0.000000000000000000, -1.000000000000000000 ) ) ;
#7514=EDGE_LOOP ( 'NONE', ( #29722, #13679, #18682, #14396, #10457, #25759, #15544, #36176, #19896, #30506, #1007, #36866 ) ) ;
#7527=DIRECTION ( 'NONE',  ( 0.000000000000000000, 0.000000000000000000, -1.000000000000000000 ) ) ;
#7566=CARTESIAN_POINT ( 'NONE',  ( 0.03113248654051816583, 0.8492681979939306069, -0.2138253033704805295 ) ) ;
#7641=FACE_OUTER_BOUND ( 'NONE', #2669, .T. ) ;
#7670=EDGE_CURVE ( 'NONE', #35412, #16124, #23076, .T. ) ;
#7682=EDGE_LOOP ( 'NONE', ( #9132, #21417, #27998, #36314, #36221 ) ) ;
#7725=EDGE_CURVE ( 'NONE', #38276, #3878, #7816, .T. ) ;
#7748=ORIENTED_EDGE ( 'NONE', *, *, #37298, .T. ) ;
#7777=DIRECTION ( 'NONE',  ( -0.4999999999999978351, -3.389636702121520322E-32, 0.8660254037844398178 ) ) ;
#7794=SHAPE_REPRESENTATION ( 'Lower cage plate', ( #27819 ), #37726 ) ;
#7816=LINE ( 'NONE', #14206, #38133 ) ;
#7881=VERTEX_POINT ( 'NONE', #6155 ) ;
#7887=EDGE_CURVE ( 'NONE', #14824, #26774, #27981, .T. ) ;
#7898=LINE ( 'NONE', #14480, #8106 ) ;
#7917=DIRECTION ( 'NONE',  ( -1.848892746611746419E-32, -0.5237184928541297468, 0.8518913899333638851 ) ) ;
#7927=FACE_BOUND ( 'NONE', #40053, .T. ) ;
#7929=VERTEX_POINT ( 'NONE', #9051 ) ;
#7961=AXIS2_PLACEMENT_3D ( 'NONE', #27547, #30632, #40279 ) ;
#7967=EDGE_LOOP ( 'NONE', ( #20031, #19222, #24335, #11289 ) ) ;
#7970=LINE ( 'NONE', #2434, #11450 ) ;
#7993=AXIS2_PLACEMENT_3D ( 'NONE', #31894, #31293, #3104 ) ;
#8001=LINE ( 'NONE', #23268, #22015 ) ;
#8013=CARTESIAN_POINT ( 'NONE',  ( 0.05999999999999990757, 0.6655791756086271160, -0.3865134954953678426 ) ) ;
#8033=EDGE_CURVE ( 'NONE', #35412, #7881, #9659, .T. ) ;
#8052=VECTOR ( 'NONE', #21724, 39.37007874015748143 ) ;
#8070=AXIS2_PLACEMENT_3D ( 'NONE', #20876, #33397, #4403 ) ;
#8106=VECTOR ( 'NONE', #36289, 39.37007874015748143 ) ;
#8108=DIRECTION ( 'NONE',  ( 1.000000000000000000, 6.779273404243070203E-32, 4.314083075427408311E-32 ) ) ;
#8161=CARTESIAN_POINT ( 'NONE',  ( 0.05999999999999990757, -0.4204378267473924402, -0.3721750714917929637 ) ) ;
#8168=EDGE_CURVE ( 'NONE', #26563, #25089, #19927, .T. ) ;
#8200=EDGE_LOOP ( 'NONE', ( #39620, #10329, #30905, #1951 ) ) ;
#8210=CARTESIAN_POINT ( 'NONE',  ( 0.03113248654051816583, 0.000000000000000000, 0.000000000000000000 ) ) ;
#8223=EDGE_CURVE ( 'NONE', #5597, #37863, #26514, .T. ) ;
#8274=ADVANCED_FACE ( 'NONE', ( #17841 ), #14352, .F. ) ;
#8290=ORIENTED_EDGE ( 'NONE', *, *, #8223, .T. ) ;
#8312=AXIS2_PLACEMENT_3D ( 'NONE', #1962, #13864, #35899 ) ;
#8315=DIRECTION ( 'NONE',  ( 1.000000000000000000, 0.000000000000000000, 0.000000000000000000 ) ) ;
#8345=EDGE_LOOP ( 'NONE', ( #30295, #15069, #26923, #35707 ) ) ;
#8385=ORIENTED_EDGE ( 'NONE', *, *, #1717, .F. ) ;
#8389=EDGE_LOOP ( 'NONE', ( #22807, #5800, #33276, #12917 ) ) ;
#8415=DIRECTION ( 'NONE',  ( -1.000000000000000000, -7.857794173099924470E-32, -8.628166150854818811E-32 ) ) ;
#8458=DIRECTION ( 'NONE',  ( -6.162975822039154046E-33, 0.000000000000000000, -1.000000000000000000 ) ) ;
#8470=EDGE_CURVE ( 'NONE', #23080, #22141, #21367, .T. ) ;
#8472=EDGE_CURVE ( 'NONE', #1162, #24445, #18450, .T. ) ;
#8543=ORIENTED_EDGE ( 'NONE', *, *, #3885, .F. ) ;
#8584=VECTOR ( 'NONE', #2433, 39.37007874015748143 ) ;
#8589=VECTOR ( 'NONE', #37271, 39.37007874015748143 ) ;
#8620=CARTESIAN_POINT ( 'NONE',  ( 0.05999999999999990757, -0.1354409211049039941, -0.1857769145426272639 ) ) ;
#8657=CYLINDRICAL_SURFACE ( 'NONE', #10199, 0.4614999999999880864 ) ;
#8670=DIRECTION ( 'NONE',  ( -1.000000000000000000, -7.857794173099924470E-32, -8.628166150854818811E-32 ) ) ;
#8681=VERTEX_POINT ( 'NONE', #6912 ) ;
#8685=DIRECTION ( 'NONE',  ( -1.000000000000000000, -7.857794173099924470E-32, -8.628166150854818811E-32 ) ) ;
#8779=VERTEX_POINT ( 'NONE', #38182 ) ;
#8800=ORIENTED_EDGE ( 'NONE', *, *, #20792, .F. ) ;
#8840=AXIS2_PLACEMENT_3D ( 'NONE', #13594, #37665, #19162 ) ;
#8860=CARTESIAN_POINT ( 'NONE',  ( 0.000000000000000000, 0.000000000000000000, 0.000000000000000000 ) ) ;
#8861=DIRECTION ( 'NONE',  ( -6.162975822039154046E-33, 0.000000000000000000, -1.000000000000000000 ) ) ;
#8920=CARTESIAN_POINT ( 'NONE',  ( 0.000000000000000000, 0.000000000000000000, 0.000000000000000000 ) ) ;
#8931=LINE ( 'NONE', #3355, #4386 ) ;
#8960=CARTESIAN_POINT ( 'NONE',  ( 0.000000000000000000, 0.8492681979939306069, -0.2138253033704803907 ) ) ;
#8965=CARTESIAN_POINT ( 'NONE',  ( 0.05999999999999990757, -0.03575622569115821658, -0.2978615321325044363 ) ) ;
#9009=CIRCLE ( 'NONE', #19533, 0.06250000000000000000 ) ;
#9044=DIRECTION ( 'NONE',  ( -0.3961231183188297922, 0.000000000000000000, 0.9181974053183586948 ) ) ;
#9051=CARTESIAN_POINT ( 'NONE',  ( -2.696301922142129510E-33, 0.7171888913565960255, -0.2325238883388469069 ) ) ;
#9094=ORIENTED_EDGE ( 'NONE', *, *, #38831, .F. ) ;
#9128=ORIENTED_EDGE ( 'NONE', *, *, #3207, .T. ) ;
#9132=ORIENTED_EDGE ( 'NONE', *, *, #32275, .F. ) ;
#9190=DIRECTION ( 'NONE',  ( 0.000000000000000000, 0.000000000000000000, -1.000000000000000000 ) ) ;
#9210=CARTESIAN_POINT ( 'NONE',  ( 0.05999999999999990757, 0.000000000000000000, 0.000000000000000000 ) ) ;
#9242=CARTESIAN_POINT ( 'NONE',  ( 0.05999999999999990757, 0.000000000000000000, 0.000000000000000000 ) ) ;
#9265=VECTOR ( 'NONE', #2826, 39.37007874015748143 ) ;
#9351=CONICAL_SURFACE ( 'NONE', #225, 0.1499999999999989675, 1.047197551196599408 ) ;
#9358=DIRECTION ( 'NONE',  ( -1.000000000000000000, -7.857794173099924470E-32, -8.628166150854818811E-32 ) ) ;
#9368=EDGE_CURVE ( 'NONE', #553, #31435, #27631, .T. ) ;
#9412=ORIENTED_EDGE ( 'NONE', *, *, #4363, .T. ) ;
#9451=LINE ( 'NONE', #24903, #39018 ) ;
#9505=CONICAL_SURFACE ( 'NONE', #33146, 0.1500000000000009659, 1.047197551196599186 ) ;
#9555=ORIENTED_EDGE ( 'NONE', *, *, #19530, .F. ) ;
#9560=DIRECTION ( 'NONE',  ( 0.000000000000000000, 0.000000000000000000, 1.000000000000000000 ) ) ;
#9608=CARTESIAN_POINT ( 'NONE',  ( 0.000000000000000000, -0.02383748379410547888, -0.1985743547550029575 ) ) ;
#9616=VERTEX_POINT ( 'NONE', #32930 ) ;
#9659=LINE ( 'NONE', #13742, #740 ) ;
#9668=ADVANCED_FACE ( 'NONE', ( #1107 ), #29454, .F. ) ;
#9681=ADVANCED_FACE ( 'NONE', ( #7641 ), #30326, .F. ) ;
#9778=EDGE_CURVE ( 'NONE', #7881, #14101, #24116, .T. ) ;
#9788=LINE ( 'NONE', #18869, #13991 ) ;
#9791=CARTESIAN_POINT ( 'NONE',  ( 0.05999999999999990757, -0.004731704300309400382, -0.008387989767859833218 ) ) ;
#9864=CARTESIAN_POINT ( 'NONE',  ( -2.696301922142130194E-33, -2.357338251929976383E-33, 0.06250000000000000000 ) ) ;
#9866=ORIENTED_EDGE ( 'NONE', *, *, #32275, .T. ) ;
#9878=DIRECTION ( 'NONE',  ( 0.000000000000000000, 0.000000000000000000, -1.000000000000000000 ) ) ;
#9880=AXIS2_PLACEMENT_3D ( 'NONE', #26677, #16587, #39211 ) ;
#9897=ORIENTED_EDGE ( 'NONE', *, *, #10296, .F. ) ;
#9907=ORIENTED_EDGE ( 'NONE', *, *, #18860, .T. ) ;
#9953=EDGE_LOOP ( 'NONE', ( #22124, #17761, #3971, #1684 ) ) ;
#9954=ORIENTED_EDGE ( 'NONE', *, *, #36038, .F. ) ;
#9989=EDGE_CURVE ( 'NONE', #39766, #31435, #25940, .T. ) ;
#10005=CIRCLE ( 'NONE', #39568, 0.6114999999999938263 ) ;
#10010=CARTESIAN_POINT ( 'NONE',  ( 0.05999999999999990757, 0.000000000000000000, 0.000000000000000000 ) ) ;
#10024=CARTESIAN_POINT ( 'NONE',  ( 0.000000000000000000, 0.7171888913565960255, -0.2950238883388468514 ) ) ;
#10026=ORIENTED_EDGE ( 'NONE', *, *, #10262, .T. ) ;
#10027=DIRECTION ( 'NONE',  ( 0.000000000000000000, 0.000000000000000000, 1.000000000000000000 ) ) ;
#10035=VECTOR ( 'NONE', #4364, 39.37007874015748143 ) ;
#10088=DIRECTION ( 'NONE',  ( -6.162975822039154730E-33, 0.000000000000000000, -1.000000000000000000 ) ) ;
#10162=DIRECTION ( 'NONE',  ( 1.000000000000000000, 6.779273404243070203E-32, 4.314083075427408311E-32 ) ) ;
#10168=EDGE_CURVE ( 'NONE', #22389, #16113, #11287, .T. ) ;
#10199=AXIS2_PLACEMENT_3D ( 'NONE', #5579, #40131, #21452 ) ;
#10238=ORIENTED_EDGE ( 'NONE', *, *, #7670, .F. ) ;
#10262=EDGE_CURVE ( 'NONE', #32272, #15843, #19607, .T. ) ;
#10273=DIRECTION ( 'NONE',  ( -6.162975822039149256E-32, 0.5237184928541297468, -0.8518913899333639961 ) ) ;
#10278=DIRECTION ( 'NONE',  ( -4.930380657631323784E-32, -0.7472307839325097456, -0.6645646360916347417 ) ) ;
#10279=EDGE_LOOP ( 'NONE', ( #21927, #11927 ) ) ;
#10286=AXIS2_PLACEMENT_3D ( 'NONE', #30624, #38627, #16841 ) ;
#10288=ORIENTED_EDGE ( 'NONE', *, *, #20334, .F. ) ;
#10296=EDGE_CURVE ( 'NONE', #15679, #31508, #4546, .T. ) ;
#10329=ORIENTED_EDGE ( 'NONE', *, *, #10456, .F. ) ;
#10388=CARTESIAN_POINT ( 'NONE',  ( 0.05999999999999990757, -0.3458405862425447119, -0.1052451372150005060 ) ) ;
#10390=CYLINDRICAL_SURFACE ( 'NONE', #22071, 0.6114999999999938263 ) ;
#10432=ORIENTED_EDGE ( 'NONE', *, *, #32108, .T. ) ;
#10456=EDGE_CURVE ( 'NONE', #10562, #16113, #29062, .T. ) ;
#10457=ORIENTED_EDGE ( 'NONE', *, *, #20738, .T. ) ;
#10469=FACE_OUTER_BOUND ( 'NONE', #11692, .T. ) ;
#10528=ORIENTED_EDGE ( 'NONE', *, *, #19783, .T. ) ;
#10536=CARTESIAN_POINT ( 'NONE',  ( 0.05999999999999990757, -0.1354409211049039941, -0.1857769145426272639 ) ) ;
#10537=VECTOR ( 'NONE', #10716, 39.37007874015748854 ) ;
#10562=VERTEX_POINT ( 'NONE', #27408 ) ;
#10583=LINE ( 'NONE', #26438, #33229 ) ;
#10591=VECTOR ( 'NONE', #17644, 39.37007874015748143 ) ;
#10600=CARTESIAN_POINT ( 'NONE',  ( 0.03113248654051816583, 0.1919340784543128453, -0.1767348310837237868 ) ) ;
#10615=ORIENTED_EDGE ( 'NONE', *, *, #37405, .F. ) ;
#10617=ORIENTED_EDGE ( 'NONE', *, *, #18426, .T. ) ;
#10665=CYLINDRICAL_SURFACE ( 'NONE', #6819, 0.4614999999999880864 ) ;
#10676=CARTESIAN_POINT ( 'NONE',  ( 0.03113248654051816583, 0.5878163732725504298, -0.2204268771689479045 ) ) ;
#10716=DIRECTION ( 'NONE',  ( 4.930380657631322689E-32, 0.7472307839325097456, 0.6645646360916346307 ) ) ;
#10717=CIRCLE ( 'NONE', #17839, 0.06250000000000001388 ) ;
#10890=DIRECTION ( 'NONE',  ( 0.000000000000000000, 0.000000000000000000, 1.000000000000000000 ) ) ;
#10927=ORIENTED_EDGE ( 'NONE', *, *, #31320, .F. ) ;
#10967=LENGTH_MEASURE_WITH_UNIT ( LENGTH_MEASURE( 0.02539999999999999897 ), #38919 );
#10971=AXIS2_PLACEMENT_3D ( 'NONE', #15792, #38205, #10027 ) ;
#10997=ORIENTED_EDGE ( 'NONE', *, *, #5104, .T. ) ;
#11018=CARTESIAN_POINT ( 'NONE',  ( 0.05999999999999990757, 0.4783370154475735103, 0.2940679337375869951 ) ) ;
#11046=CARTESIAN_POINT ( 'NONE',  ( 0.03113248654051816583, 0.3931478764542372661, 0.2416960844521746365 ) ) ;
#11054=ORIENTED_EDGE ( 'NONE', *, *, #25802, .T. ) ;
#11055=DIRECTION ( 'NONE',  ( 1.000000000000000000, 7.857794173099924470E-32, 8.628166150854818811E-32 ) ) ;
#11107=DIRECTION ( 'NONE',  ( -1.000000000000000000, -7.857794173099924470E-32, -8.628166150854818811E-32 ) ) ;
#11173=ORIENTED_EDGE ( 'NONE', *, *, #17292, .F. ) ;
#11179=AXIS2_PLACEMENT_3D ( 'NONE', #25088, #18104, #18308 ) ;
#11201=DIRECTION ( 'NONE',  ( 1.000000000000000000, 6.779273404243070203E-32, 4.314083075427408311E-32 ) ) ;
#11203=DIRECTION ( 'NONE',  ( 0.000000000000000000, 0.000000000000000000, -1.000000000000000000 ) ) ;
#11225=ORIENTED_EDGE ( 'NONE', *, *, #15033, .F. ) ;
#11231=DIRECTION ( 'NONE',  ( 1.000000000000000000, 6.779273404243070203E-32, -6.162975822039154730E-33 ) ) ;
#11248=DIRECTION ( 'NONE',  ( 0.000000000000000000, 0.000000000000000000, -1.000000000000000000 ) ) ;
#11287=LINE ( 'NONE', #23856, #19874 ) ;
#11289=ORIENTED_EDGE ( 'NONE', *, *, #30591, .F. ) ;
#11372=EDGE_LOOP ( 'NONE', ( #19122, #32608, #10927, #17300, #31501 ) ) ;
#11381=AXIS2_PLACEMENT_3D ( 'NONE', #30881, #25122, #37660 ) ;
#11388=AXIS2_PLACEMENT_3D ( 'NONE', #29389, #4659, #29179 ) ;
#11399=( GEOMETRIC_REPRESENTATION_CONTEXT ( 3 ) GLOBAL_UNCERTAINTY_ASSIGNED_CONTEXT ( ( #15737 ) ) GLOBAL_UNIT_ASSIGNED_CONTEXT ( ( #1126, #26195, #23112 ) ) REPRESENTATION_CONTEXT ( 'NONE', 'WORKASPACE' ) );
#11414=CYLINDRICAL_SURFACE ( 'NONE', #6352, 0.1000000000000000194 ) ;
#11440=ORIENTED_EDGE ( 'NONE', *, *, #9778, .F. ) ;
#11450=VECTOR ( 'NONE', #7777, 39.37007874015748143 ) ;
#11466=AXIS2_PLACEMENT_3D ( 'NONE', #18592, #30734, #27458 ) ;
#11507=EDGE_CURVE ( 'NONE', #892, #20310, #14811, .T. ) ;
#11524=AXIS2_PLACEMENT_3D ( 'NONE', #18295, #30834, #15196 ) ;
#11610=ORIENTED_EDGE ( 'NONE', *, *, #27569, .F. ) ;
#11676=DIRECTION ( 'NONE',  ( 1.000000000000000000, 6.779273404243070203E-32, 4.314083075427408311E-32 ) ) ;
#11692=EDGE_LOOP ( 'NONE', ( #33630, #1290, #18974, #30795 ) ) ;
#11699=ORIENTED_EDGE ( 'NONE', *, *, #15243, .F. ) ;
#11710=DIRECTION ( 'NONE',  ( -1.000000000000000000, -6.779273404243070203E-32, -4.314083075427408311E-32 ) ) ;
#11737=VERTEX_POINT ( 'NONE', #16628 ) ;
#11745=ORIENTED_EDGE ( 'NONE', *, *, #39859, .F. ) ;
#11757=DIRECTION ( 'NONE',  ( -1.000000000000000000, -6.779273404243070203E-32, -4.314083075427408311E-32 ) ) ;
#11771=FACE_OUTER_BOUND ( 'NONE', #16700, .T. ) ;
#11841=DIRECTION ( 'NONE',  ( 0.000000000000000000, 0.000000000000000000, -1.000000000000000000 ) ) ;
#11873=CARTESIAN_POINT ( 'NONE',  ( 0.05999999999999990757, 0.000000000000000000, 0.000000000000000000 ) ) ;
#11888=AXIS2_PLACEMENT_3D ( 'NONE', #15670, #36857, #12188 ) ;
#11917=AXIS2_PLACEMENT_3D ( 'NONE', #35219, #38500, #19389 ) ;
#11927=ORIENTED_EDGE ( 'NONE', *, *, #1717, .T. ) ;
#11951=DIRECTION ( 'NONE',  ( -3.389636702121531817E-32, 0.8709776783778059306, -0.4913225862583635584 ) ) ;
#11974=CARTESIAN_POINT ( 'NONE',  ( 0.05999999999999990757, 0.000000000000000000, 0.2000000000000000111 ) ) ;
#11988=CARTESIAN_POINT ( 'NONE',  ( 0.05999999999999990757, 0.5632502439596359656, -0.2139757610878384453 ) ) ;
#11999=EDGE_LOOP ( 'NONE', ( #32081, #37842, #33030, #32523 ) ) ;
#12005=CARTESIAN_POINT ( 'NONE',  ( 0.000000000000000000, 0.000000000000000000, 0.000000000000000000 ) ) ;
#12009=LINE ( 'NONE', #34013, #14027 ) ;
#12010=DIRECTION ( 'NONE',  ( 0.4999999999999982792, 0.6484591962157929546, 0.5740214898792285192 ) ) ;
#12015=CARTESIAN_POINT ( 'NONE',  ( 0.000000000000000000, -0.03575622569115821658, -0.2978615321325044363 ) ) ;
#12021=CARTESIAN_POINT ( 'NONE',  ( 0.05999999999999990757, 0.2954784694557334168, 0.05188905557145093855 ) ) ;
#12024=CARTESIAN_POINT ( 'NONE',  ( 0.05999999999999990757, 0.1969856463038233696, 0.03459270371430114843 ) ) ;
#12030=ORIENTED_EDGE ( 'NONE', *, *, #40432, .T. ) ;
#12041=FACE_OUTER_BOUND ( 'NONE', #25108, .T. ) ;
#12057=PRODUCT_DEFINITION_CONTEXT ( 'detailed design', #36329, 'design' ) ;
#12071=AXIS2_PLACEMENT_3D ( 'NONE', #17236, #11676, #30395 ) ;
#12107=ORIENTED_EDGE ( 'NONE', *, *, #8470, .T. ) ;
#12112=VECTOR ( 'NONE', #9358, 39.37007874015748143 ) ;
#12134=ORIENTED_EDGE ( 'NONE', *, *, #38921, .T. ) ;
#12152=AXIS2_PLACEMENT_3D ( 'NONE', #660, #22650, #34964 ) ;
#12156=CIRCLE ( 'NONE', #39080, 0.2000000000000000389 ) ;
#12188=DIRECTION ( 'NONE',  ( 0.000000000000000000, 0.000000000000000000, -1.000000000000000000 ) ) ;
#12219=CARTESIAN_POINT ( 'NONE',  ( 0.03113248654051816583, -0.4578766358967566452, -0.4053162176620345170 ) ) ;
#12223=DIRECTION ( 'NONE',  ( -1.000000000000000000, -7.857794173099924470E-32, -8.628166150854818811E-32 ) ) ;
#12251=DIRECTION ( 'NONE',  ( 1.000000000000000000, 6.779273404243070203E-32, 4.314083075427408311E-32 ) ) ;
#12253=EDGE_LOOP ( 'NONE', ( #9555, #20640, #28872, #25322 ) ) ;
#12254=AXIS2_PLACEMENT_3D ( 'NONE', #39792, #5024, #32603 ) ;
#12270=ORIENTED_EDGE ( 'NONE', *, *, #1477, .T. ) ;
#12286=ORIENTED_EDGE ( 'NONE', *, *, #33445, .F. ) ;
#12288=DIRECTION ( 'NONE',  ( 0.000000000000000000, 0.000000000000000000, -1.000000000000000000 ) ) ;
#12315=ORIENTED_EDGE ( 'NONE', *, *, #30679, .T. ) ;
#12429=EDGE_LOOP ( 'NONE', ( #39762, #10026, #28730, #30448 ) ) ;
#12432=CARTESIAN_POINT ( 'NONE',  ( 0.03113248654051816583, -0.3458405862425447119, -0.1052451372150005060 ) ) ;
#12464=CARTESIAN_POINT ( 'NONE',  ( 0.03113248654051816583, -0.02383748379410547888, -0.1985743547550029575 ) ) ;
#12491=ORIENTED_EDGE ( 'NONE', *, *, #34164, .T. ) ;
#12498=AXIS2_PLACEMENT_3D ( 'NONE', #21418, #18716, #30659 ) ;
#12567=VECTOR ( 'NONE', #15270, 39.37007874015748143 ) ;
#12588=AXIS2_PLACEMENT_3D ( 'NONE', #29041, #38702, #909 ) ;
#12638=VECTOR ( 'NONE', #36229, 39.37007874015748143 ) ;
#12648=DIRECTION ( 'NONE',  ( 1.000000000000000000, 6.779273404243070203E-32, 4.314083075427408311E-32 ) ) ;
#12711=CIRCLE ( 'NONE', #1571, 0.6114999999999938263 ) ;
#12735=DIRECTION ( 'NONE',  ( 0.4999999999999984457, 3.389636702121524701E-32, -0.8660254037844394848 ) ) ;
#12778=FACE_OUTER_BOUND ( 'NONE', #11372, .T. ) ;
#12781=FACE_OUTER_BOUND ( 'NONE', #5727, .T. ) ;
#12794=LINE ( 'NONE', #28637, #38804 ) ;
#12804=AXIS2_PLACEMENT_3D ( 'NONE', #9791, #38376, #3627 ) ;
#12843=DIRECTION ( 'NONE',  ( 0.000000000000000000, 0.000000000000000000, -1.000000000000000000 ) ) ;
#12917=ORIENTED_EDGE ( 'NONE', *, *, #26536, .F. ) ;
#12928=CARTESIAN_POINT ( 'NONE',  ( 0.05999999999999990757, 0.4357424459509064985, 0.2678820090948821342 ) ) ;
#12947=EDGE_CURVE ( 'NONE', #14789, #30962, #3037, .T. ) ;
#12985=APPLICATION_CONTEXT ( 'configuration controlled 3d designs of mechanical parts and assemblies' ) ;
#13109=FACE_OUTER_BOUND ( 'NONE', #13457, .T. ) ;
#13130=DIRECTION ( 'NONE',  ( 1.000000000000000000, 6.779273404243070203E-32, 4.314083075427408311E-32 ) ) ;
#13166=CARTESIAN_POINT ( 'NONE',  ( 0.03113248654051816583, -0.1960639381401260983, -0.03948331496955503200 ) ) ;
#13214=CIRCLE ( 'NONE', #36199, 0.1500000000000009659 ) ;
#13274=DIRECTION ( 'NONE',  ( -1.000000000000000000, -7.857794173099924470E-32, -8.628166150854818811E-32 ) ) ;
#13298=DIRECTION ( 'NONE',  ( 1.000000000000000000, 6.779273404243070203E-32, 4.314083075427408311E-32 ) ) ;
#13303=ORIENTED_EDGE ( 'NONE', *, *, #38831, .T. ) ;
#13323=DIRECTION ( 'NONE',  ( -1.000000000000000000, -7.857794173099924470E-32, -8.628166150854818811E-32 ) ) ;
#13444=CIRCLE ( 'NONE', #24625, 0.5114999999999890745 ) ;
#13445=CONICAL_SURFACE ( 'NONE', #37761, 0.5614999999999926716, 1.047197551196600296 ) ;
#13457=EDGE_LOOP ( 'NONE', ( #23889, #5486, #29999, #9128 ) ) ;
#13474=VECTOR ( 'NONE', #19141, 39.37007874015748143 ) ;
#13568=EDGE_LOOP ( 'NONE', ( #38090, #25385, #1098, #5541 ) ) ;
#13587=CARTESIAN_POINT ( 'NONE',  ( 0.000000000000000000, 0.000000000000000000, 0.000000000000000000 ) ) ;
#13594=CARTESIAN_POINT ( 'NONE',  ( 0.05999999999999990757, 0.000000000000000000, 0.000000000000000000 ) ) ;
#13601=CARTESIAN_POINT ( 'NONE',  ( 0.000000000000000000, 0.000000000000000000, 0.000000000000000000 ) ) ;
#13651=EDGE_CURVE ( 'NONE', #5233, #34649, #23665, .T. ) ;
#13662=ORIENTED_EDGE ( 'NONE', *, *, #26536, .T. ) ;
#13663=VERTEX_POINT ( 'NONE', #35587 ) ;
#13679=ORIENTED_EDGE ( 'NONE', *, *, #22792, .T. ) ;
#13695=EDGE_CURVE ( 'NONE', #34438, #14824, #8001, .T. ) ;
#13712=VERTEX_POINT ( 'NONE', #5116 ) ;
#13742=CARTESIAN_POINT ( 'NONE',  ( 0.05999999999999990757, -0.2793841226333812489, -0.1799682156082512696 ) ) ;
#13743=CARTESIAN_POINT ( 'NONE',  ( 0.03113248654051816583, 0.5632502439596359656, -0.2139757610878384453 ) ) ;
#13801=CARTESIAN_POINT ( 'NONE',  ( 0.000000000000000000, 0.1919340784543128453, -0.1767348310837237868 ) ) ;
#13802=DIRECTION ( 'NONE',  ( -6.162975822039154046E-33, 0.000000000000000000, -1.000000000000000000 ) ) ;
#13835=ORIENTED_EDGE ( 'NONE', *, *, #3753, .F. ) ;
#13864=DIRECTION ( 'NONE',  ( 1.000000000000000000, 6.779273404243070203E-32, 4.314083075427408311E-32 ) ) ;
#13869=LINE ( 'NONE', #1782, #14035 ) ;
#13879=AXIS2_PLACEMENT_3D ( 'NONE', #10024, #3838, #31838 ) ;
#13890=FACE_BOUND ( 'NONE', #7514, .T. ) ;
#13991=VECTOR ( 'NONE', #24840, 39.37007874015748143 ) ;
#14000=EDGE_CURVE ( 'NONE', #25089, #40017, #13444, .T. ) ;
#14010=DIRECTION ( 'NONE',  ( 0.000000000000000000, 0.000000000000000000, -1.000000000000000000 ) ) ;
#14011=EDGE_LOOP ( 'NONE', ( #40493, #9094 ) ) ;
#14027=VECTOR ( 'NONE', #30924, 39.37007874015747433 ) ;
#14035=VECTOR ( 'NONE', #20078, 39.37007874015748143 ) ;
#14044=CARTESIAN_POINT ( 'NONE',  ( 0.03113248654051816583, -0.1022126893003200560, -0.2231384537392532841 ) ) ;
#14047=AXIS2_PLACEMENT_3D ( 'NONE', #23405, #1378, #23593 ) ;
#14101=VERTEX_POINT ( 'NONE', #180 ) ;
#14103=FACE_OUTER_BOUND ( 'NONE', #5, .T. ) ;
#14109=CARTESIAN_POINT ( 'NONE',  ( 0.03113248654051816583, 0.000000000000000000, 0.000000000000000000 ) ) ;
#14130=FACE_OUTER_BOUND ( 'NONE', #29526, .T. ) ;
#14134=CARTESIAN_POINT ( 'NONE',  ( 0.000000000000000000, 0.5209315849442416324, 0.3202538583802939098 ) ) ;
#14158=CARTESIAN_POINT ( 'NONE',  ( 0.03113248654051816583, 0.1997995745459845707, -0.008951536808938304751 ) ) ;
#14167=ADVANCED_FACE ( 'NONE', ( #22174 ), #6492, .T. ) ;
#14206=CARTESIAN_POINT ( 'NONE',  ( 0.05999999999999990757, 0.07140090991423790612, -0.1319162994607513684 ) ) ;
#14212=ADVANCED_BREP_SHAPE_REPRESENTATION ( '', ( #18866, #27819 ), #37726 ) ;
#14295=DIRECTION ( 'NONE',  ( -1.000000000000000000, -7.857794173099924470E-32, -8.628166150854818811E-32 ) ) ;
#14322=FACE_BOUND ( 'NONE', #10279, .T. ) ;
#14329=DIRECTION ( 'NONE',  ( -1.000000000000000000, -7.857794173099924470E-32, -8.628166150854818811E-32 ) ) ;
#14352=CYLINDRICAL_SURFACE ( 'NONE', #28298, 0.06250000000000000000 ) ;
#14394=ORIENTED_EDGE ( 'NONE', *, *, #29609, .F. ) ;
#14396=ORIENTED_EDGE ( 'NONE', *, *, #20792, .T. ) ;
#14421=LINE ( 'NONE', #29881, #36385 ) ;
#14447=ORIENTED_EDGE ( 'NONE', *, *, #7887, .F. ) ;
#14480=CARTESIAN_POINT ( 'NONE',  ( 0.05999999999999990757, -0.01787811284557883421, -0.1489307660662511357 ) ) ;
#14481=CARTESIAN_POINT ( 'NONE',  ( 0.000000000000000000, 0.5878163732725504298, -0.1704268771689479434 ) ) ;
#14502=DIRECTION ( 'NONE',  ( 0.000000000000000000, 0.000000000000000000, -1.000000000000000000 ) ) ;
#14609=DIRECTION ( 'NONE',  ( 0.000000000000000000, 0.000000000000000000, 1.000000000000000000 ) ) ;
#14658=VERTEX_POINT ( 'NONE', #38325 ) ;
#14701=ORIENTED_EDGE ( 'NONE', *, *, #19648, .F. ) ;
#14779=CIRCLE ( 'NONE', #17421, 0.1000000000000000194 ) ;
#14789=VERTEX_POINT ( 'NONE', #26624 ) ;
#14810=AXIS2_PLACEMENT_3D ( 'NONE', #2912, #22261, #9878 ) ;
#14811=LINE ( 'NONE', #5928, #26489 ) ;
#14824=VERTEX_POINT ( 'NONE', #14044 ) ;
#14895=VECTOR ( 'NONE', #39134, 39.37007874015748143 ) ;
#14897=DIRECTION ( 'NONE',  ( 0.4999999999999982792, 0.4254978411528176907, 0.7542887956043713427 ) ) ;
#14906=ADVANCED_FACE ( 'NONE', ( #11771 ), #2327, .F. ) ;
#14917=ADVANCED_FACE ( 'NONE', ( #30898 ), #19790, .F. ) ;
#14925=DIRECTION ( 'NONE',  ( -6.162975822039154730E-33, 0.000000000000000000, -1.000000000000000000 ) ) ;
#14945=CYLINDRICAL_SURFACE ( 'NONE', #22011, 0.06249999999999997918 ) ;
#14966=EDGE_CURVE ( 'NONE', #14101, #1197, #5377, .T. ) ;
#14972=LINE ( 'NONE', #14158, #2233 ) ;
#14974=DIRECTION ( 'NONE',  ( -1.000000000000000000, -6.779273404243070203E-32, -4.314083075427408311E-32 ) ) ;
#15033=EDGE_CURVE ( 'NONE', #37863, #37734, #12794, .T. ) ;
#15044=CARTESIAN_POINT ( 'NONE',  ( 0.03113248654051816583, 0.2954784694557334168, 0.05188905557145093855 ) ) ;
#15048=DIRECTION ( 'NONE',  ( 1.000000000000000000, 6.779273404243070203E-32, 4.314083075427408311E-32 ) ) ;
#15069=ORIENTED_EDGE ( 'NONE', *, *, #28018, .T. ) ;
#15106=ORIENTED_EDGE ( 'NONE', *, *, #20623, .F. ) ;
#15144=VECTOR ( 'NONE', #1503, 39.37007874015748854 ) ;
#15196=DIRECTION ( 'NONE',  ( -0.4413459890218813797, -0.8973370147131440877, 0.000000000000000000 ) ) ;
#15200=AXIS2_PLACEMENT_3D ( 'NONE', #34311, #18687, #18285 ) ;
#15222=DIRECTION ( 'NONE',  ( 0.000000000000000000, 0.000000000000000000, 1.000000000000000000 ) ) ;
#15229=CIRCLE ( 'NONE', #7302, 0.06250000000000000000 ) ;
#15243=EDGE_CURVE ( 'NONE', #199, #30962, #20947, .T. ) ;
#15264=EDGE_LOOP ( 'NONE', ( #38986, #2877, #36977, #251 ) ) ;
#15270=DIRECTION ( 'NONE',  ( -1.000000000000000000, -6.779273404243070203E-32, -4.314083075427407763E-32 ) ) ;
#15328=CARTESIAN_POINT ( 'NONE',  ( 0.000000000000000000, 0.09520121321898405986, -0.1758883992810029440 ) ) ;
#15362=AXIS2_PLACEMENT_3D ( 'NONE', #37225, #27763, #2273 ) ;
#15400=AXIS2_PLACEMENT_3D ( 'NONE', #8210, #11710, #33308 ) ;
#15409=VECTOR ( 'NONE', #31513, 39.37007874015748854 ) ;
#15468=CARTESIAN_POINT ( 'NONE',  ( 0.05999999999999990757, 0.1477392347278677909, 0.02594452778572553867 ) ) ;
#15524=ORIENTED_EDGE ( 'NONE', *, *, #7670, .T. ) ;
#15544=ORIENTED_EDGE ( 'NONE', *, *, #5096, .T. ) ;
#15577=CARTESIAN_POINT ( 'NONE',  ( 0.05999999999999990757, 0.000000000000000000, 0.000000000000000000 ) ) ;
#15616=PLANE ( 'NONE',  #11524 ) ;
#15665=DIRECTION ( 'NONE',  ( 1.000000000000000000, 6.779273404243070203E-32, 4.314083075427408311E-32 ) ) ;
#15670=CARTESIAN_POINT ( 'NONE',  ( 0.05999999999999990757, -0.3458405862425447119, -0.1052451372150005060 ) ) ;
#15679=VERTEX_POINT ( 'NONE', #24382 ) ;
#15695=DIRECTION ( 'NONE',  ( 1.000000000000000000, 6.779273404243070203E-32, 4.314083075427408311E-32 ) ) ;
#15724=CARTESIAN_POINT ( 'NONE',  ( 0.05999999999999990757, 0.000000000000000000, 0.000000000000000000 ) ) ;
#15737=UNCERTAINTY_MEASURE_WITH_UNIT (LENGTH_MEASURE( 1.000000000000000082E-05 ), #1126, 'distance_accuracy_value', 'NONE');
#15768=ORIENTED_EDGE ( 'NONE', *, *, #13695, .T. ) ;
#15792=CARTESIAN_POINT ( 'NONE',  ( 0.05999999999999990757, 0.000000000000000000, 0.000000000000000000 ) ) ;
#15843=VERTEX_POINT ( 'NONE', #6861 ) ;
#15888=CARTESIAN_POINT ( 'NONE',  ( 0.03113248654051816583, -0.2793841226333812489, -0.1799682156082512696 ) ) ;
#15914=LINE ( 'NONE', #12024, #39229 ) ;
#16011=LINE ( 'NONE', #12928, #22449 ) ;
#16013=VECTOR ( 'NONE', #10273, 39.37007874015748143 ) ;
#16018=LINE ( 'NONE', #31852, #35849 ) ;
#16041=CARTESIAN_POINT ( 'NONE',  ( 0.05999999999999990757, -0.0007915077497714572644, 0.0008899645335182150997 ) ) ;
#16056=CARTESIAN_POINT ( 'NONE',  ( 0.03113248654051816583, 0.1919340784543128453, -0.1767348310837237868 ) ) ;
#16061=ORIENTED_EDGE ( 'NONE', *, *, #5769, .T. ) ;
#16093=ORIENTED_EDGE ( 'NONE', *, *, #19551, .F. ) ;
#16105=CARTESIAN_POINT ( 'NONE',  ( 0.03113248654051816583, 0.2463462108298974940, -0.03520871226632921180 ) ) ;
#16113=VERTEX_POINT ( 'NONE', #16105 ) ;
#16124=VERTEX_POINT ( 'NONE', #28646 ) ;
#16178=DIRECTION ( 'NONE',  ( 0.000000000000000000, -0.5237184928541299689, 0.8518913899333638851 ) ) ;
#16222=CARTESIAN_POINT ( 'NONE',  ( 0.05999999999999990757, 0.7171888913565960255, -0.2325238883388469069 ) ) ;
#16239=CARTESIAN_POINT ( 'NONE',  ( 0.05999999999999990757, 0.03243672405480754750, -0.03647157466310641666 ) ) ;
#16275=ADVANCED_FACE ( 'NONE', ( #40317 ), #6162, .T. ) ;
#16459=CARTESIAN_POINT ( 'NONE',  ( 0.05999999999999990757, 0.4357424459509059433, 0.2678820090948816901 ) ) ;
#16470=CYLINDRICAL_SURFACE ( 'NONE', #8840, 0.2000000000000000111 ) ;
#16501=VECTOR ( 'NONE', #38446, 39.37007874015748143 ) ;
#16555=AXIS2_PLACEMENT_3D ( 'NONE', #24877, #25065, #36995 ) ;
#16587=DIRECTION ( 'NONE',  ( -1.000000000000000000, -7.857794173099924470E-32, -8.628166150854818811E-32 ) ) ;
#16591=ADVANCED_FACE ( 'NONE', ( #10469 ), #1521, .T. ) ;
#16606=ORIENTED_EDGE ( 'NONE', *, *, #6121, .T. ) ;
#16628=CARTESIAN_POINT ( 'NONE',  ( 0.000000000000000000, 0.5632502439596359656, -0.2139757610878384453 ) ) ;
#16648=ORIENTED_EDGE ( 'NONE', *, *, #30591, .T. ) ;
#16700=EDGE_LOOP ( 'NONE', ( #16606, #17087, #23943, #9897 ) ) ;
#16701=EDGE_CURVE ( 'NONE', #32303, #32272, #10717, .T. ) ;
#16715=LINE ( 'NONE', #7430, #15144 ) ;
#16753=ORIENTED_EDGE ( 'NONE', *, *, #23245, .F. ) ;
#16779=EDGE_CURVE ( 'NONE', #32303, #7929, #19031, .T. ) ;
#16791=ORIENTED_EDGE ( 'NONE', *, *, #3885, .T. ) ;
#16805=CARTESIAN_POINT ( 'NONE',  ( 0.03113248654051816583, 0.8492681979939306069, -0.2138253033704805295 ) ) ;
#16807=LINE ( 'NONE', #4830, #25257 ) ;
#16830=CIRCLE ( 'NONE', #39804, 0.1499999999999990785 ) ;
#16831=AXIS2_PLACEMENT_3D ( 'NONE', #38922, #26392, #23326 ) ;
#16841=DIRECTION ( 'NONE',  ( 0.000000000000000000, 0.000000000000000000, 1.000000000000000000 ) ) ;
#16859=ORIENTED_EDGE ( 'NONE', *, *, #39388, .T. ) ;
#16883=CARTESIAN_POINT ( 'NONE',  ( 0.05999999999999990757, 0.6304109427692223822, -0.1442409525262416947 ) ) ;
#16997=CYLINDRICAL_SURFACE ( 'NONE', #34432, 0.1000000000000000056 ) ;
#17016=CARTESIAN_POINT ( 'NONE',  ( 0.05999999999999990757, 0.000000000000000000, 0.000000000000000000 ) ) ;
#17043=VERTEX_POINT ( 'NONE', #17078 ) ;
#17071=DIRECTION ( 'NONE',  ( 1.000000000000000000, 6.779273404243070203E-32, 4.314083075427407763E-32 ) ) ;
#17076=FACE_OUTER_BOUND ( 'NONE', #25181, .T. ) ;
#17078=CARTESIAN_POINT ( 'NONE',  ( 0.05999999999999990757, 7.654042494670954463E-18, -0.06250000000000000000 ) ) ;
#17081=AXIS2_PLACEMENT_3D ( 'NONE', #9210, #6122, #18475 ) ;
#17087=ORIENTED_EDGE ( 'NONE', *, *, #29614, .F. ) ;
#17103=DIRECTION ( 'NONE',  ( 1.000000000000000000, 6.779273404243070203E-32, 4.314083075427408311E-32 ) ) ;
#17105=EDGE_LOOP ( 'NONE', ( #10615, #2350, #7191, #35038 ) ) ;
#17111=DIRECTION ( 'NONE',  ( 2.157041537713702240E-32, -0.8709776783778059306, 0.4913225862583635584 ) ) ;
#17159=DIRECTION ( 'NONE',  ( 0.000000000000000000, -2.731847993664239947E-15, -1.000000000000000000 ) ) ;
#17194=VECTOR ( 'NONE', #11951, 39.37007874015748143 ) ;
#17236=CARTESIAN_POINT ( 'NONE',  ( 0.03113248654051816583, -0.2940959072101921867, -0.05922497245433272495 ) ) ;
#17248=DIRECTION ( 'NONE',  ( 0.000000000000000000, 0.000000000000000000, -1.000000000000000000 ) ) ;
#17292=EDGE_CURVE ( 'NONE', #38276, #9616, #37541, .T. ) ;
#17300=ORIENTED_EDGE ( 'NONE', *, *, #28811, .F. ) ;
#17362=AXIS2_PLACEMENT_3D ( 'NONE', #23584, #22965, #7509 ) ;
#17383=DIRECTION ( 'NONE',  ( -0.4413459890218811021, 0.8973370147131440877, 0.000000000000000000 ) ) ;
#17384=LINE ( 'NONE', #36095, #23894 ) ;
#17399=CIRCLE ( 'NONE', #12152, 0.2000000000000000389 ) ;
#17421=AXIS2_PLACEMENT_3D ( 'NONE', #36339, #33453, #11248 ) ;
#17484=CARTESIAN_POINT ( 'NONE',  ( 0.03113248654051816583, 0.000000000000000000, 0.000000000000000000 ) ) ;
#17512=DIRECTION ( 'NONE',  ( -1.000000000000000000, -7.857794173099924470E-32, -8.628166150854818811E-32 ) ) ;
#17516=CARTESIAN_POINT ( 'NONE',  ( 0.03113248654051816583, -0.3767386922704979990, -0.2665524483967541269 ) ) ;
#17556=CIRCLE ( 'NONE', #31997, 0.4614999999999880864 ) ;
#17562=EDGE_LOOP ( 'NONE', ( #30228, #21698, #18122, #5429, #25250 ) ) ;
#17592=DIRECTION ( 'NONE',  ( -6.162975822039152677E-33, 0.000000000000000000, -1.000000000000000000 ) ) ;
#17611=CARTESIAN_POINT ( 'NONE',  ( 0.05999999999999990757, -0.3829990175980249600, -0.3390339253215535198 ) ) ;
#17613=CARTESIAN_POINT ( 'NONE',  ( 0.03113248654051816583, -0.03575622569115821658, -0.2978615321325044363 ) ) ;
#17644=DIRECTION ( 'NONE',  ( 6.779273404243062539E-32, -0.5237184928541297468, 0.8518913899333639961 ) ) ;
#17650=ORIENTED_EDGE ( 'NONE', *, *, #9368, .T. ) ;
#17653=ORIENTED_EDGE ( 'NONE', *, *, #38860, .F. ) ;
#17673=LINE ( 'NONE', #5309, #1486 ) ;
#17681=ADVANCED_FACE ( 'NONE', ( #36606 ), #190, .F. ) ;
#17752=CIRCLE ( 'NONE', #8070, 0.1000000000000000194 ) ;
#17761=ORIENTED_EDGE ( 'NONE', *, *, #32098, .T. ) ;
#17772=CARTESIAN_POINT ( 'NONE',  ( 0.05999999999999990757, 0.7171888913565960255, -0.2950238883388468514 ) ) ;
#17774=PLANE ( 'NONE',  #5463 ) ;
#17839=AXIS2_PLACEMENT_3D ( 'NONE', #22142, #5501, #24247 ) ;
#17841=FACE_OUTER_BOUND ( 'NONE', #26024, .T. ) ;
#17910=VECTOR ( 'NONE', #16178, 39.37007874015748854 ) ;
#17970=DIRECTION ( 'NONE',  ( -6.162975822039154730E-33, 0.000000000000000000, -1.000000000000000000 ) ) ;
#17972=CARTESIAN_POINT ( 'NONE',  ( 0.03113248654051816583, 0.6410130462957083219, -0.4300623794142587886 ) ) ;
#17975=EDGE_CURVE ( 'NONE', #6091, #8779, #10005, .T. ) ;
#18028=ADVANCED_FACE ( 'NONE', ( #33410 ), #9351, .T. ) ;
#18074=VERTEX_POINT ( 'NONE', #15468 ) ;
#18085=CIRCLE ( 'NONE', #29242, 0.1000000000000000194 ) ;
#18104=DIRECTION ( 'NONE',  ( 1.000000000000000000, 6.779273404243070203E-32, 4.314083075427408311E-32 ) ) ;
#18122=ORIENTED_EDGE ( 'NONE', *, *, #24794, .T. ) ;
#18149=LINE ( 'NONE', #11974, #32292 ) ;
#18161=LINE ( 'NONE', #11988, #2266 ) ;
#18165=CONICAL_SURFACE ( 'NONE', #10286, 0.5614999999999926716, 1.047197551196600296 ) ;
#18269=ADVANCED_FACE ( 'NONE', ( #17076 ), #2149, .T. ) ;
#18283=ORIENTED_EDGE ( 'NONE', *, *, #36131, .F. ) ;
#18285=DIRECTION ( 'NONE',  ( 0.000000000000000000, 0.000000000000000000, -1.000000000000000000 ) ) ;
#18295=CARTESIAN_POINT ( 'NONE',  ( 0.03113248654051816583, 0.6304109427692223822, -0.1442409525262416947 ) ) ;
#18308=DIRECTION ( 'NONE',  ( 0.000000000000000000, 0.000000000000000000, -1.000000000000000000 ) ) ;
#18350=CARTESIAN_POINT ( 'NONE',  ( 0.03113248654051816583, -0.2276394436010286959, -0.1339480508475833498 ) ) ;
#18385=PLANE ( 'NONE',  #36584 ) ;
#18387=ORIENTED_EDGE ( 'NONE', *, *, #34843, .F. ) ;
#18396=ORIENTED_EDGE ( 'NONE', *, *, #16779, .T. ) ;
#18426=EDGE_CURVE ( 'NONE', #20959, #6091, #17673, .T. ) ;
#18450=LINE ( 'NONE', #18664, #9265 ) ;
#18475=DIRECTION ( 'NONE',  ( 0.000000000000000000, 0.000000000000000000, -1.000000000000000000 ) ) ;
#18487=ADVANCED_FACE ( 'NONE', ( #22409 ), #3678, .T. ) ;
#18493=DIRECTION ( 'NONE',  ( 0.4999999999999988343, 3.389636702121526891E-32, -0.8660254037844391517 ) ) ;
#18518=CIRCLE ( 'NONE', #21141, 0.04999999999999885092 ) ;
#18536=CARTESIAN_POINT ( 'NONE',  ( 0.05999999999999990757, -0.1470479536050930680, -0.02961248622716588369 ) ) ;
#18545=ADVANCED_FACE ( 'NONE', ( #35955 ), #5407, .F. ) ;
#18553=CARTESIAN_POINT ( 'NONE',  ( 0.000000000000000000, -0.3165425539888620521, -0.4137570037148034507 ) ) ;
#18555=DIRECTION ( 'NONE',  ( -0.8660254037844392627, -0.2456612931291814739, -0.4354888391889020771 ) ) ;
#18561=CARTESIAN_POINT ( 'NONE',  ( 0.03113248654051816583, 0.5878163732725504298, -0.1704268771689479434 ) ) ;
#18592=CARTESIAN_POINT ( 'NONE',  ( 0.05999999999999990757, -0.03575622569115821658, -0.2978615321325044363 ) ) ;
#18600=DIRECTION ( 'NONE',  ( 2.157041537713701966E-32, -0.8709776783778060416, 0.4913225862583635584 ) ) ;
#18605=CIRCLE ( 'NONE', #11381, 0.1000000000000000194 ) ;
#18611=EDGE_LOOP ( 'NONE', ( #14394, #22362, #38735, #12286 ) ) ;
#18648=CARTESIAN_POINT ( 'NONE',  ( 0.000000000000000000, 0.6304109427692223822, -0.1442409525262416947 ) ) ;
#18664=CARTESIAN_POINT ( 'NONE',  ( 0.05999999999999990757, 0.3931478764542372661, 0.2416960844521746365 ) ) ;
#18682=ORIENTED_EDGE ( 'NONE', *, *, #492, .T. ) ;
#18687=DIRECTION ( 'NONE',  ( 1.000000000000000000, 6.779273404243070203E-32, 4.314083075427408311E-32 ) ) ;
#18716=DIRECTION ( 'NONE',  ( -1.000000000000000000, -6.779273404243070203E-32, -4.314083075427408311E-32 ) ) ;
#18738=EDGE_LOOP ( 'NONE', ( #16061, #14447, #11610, #798 ) ) ;
#18758=LENGTH_MEASURE_WITH_UNIT ( LENGTH_MEASURE( 0.02539999999999999897 ), #25340 );
#18776=CARTESIAN_POINT ( 'NONE',  ( 0.000000000000000000, 0.1919340784543128453, -0.1767348310837237868 ) ) ;
#18832=DIRECTION ( 'NONE',  ( 1.000000000000000000, 6.779273404243070203E-32, 4.314083075427408311E-32 ) ) ;
#18844=ORIENTED_EDGE ( 'NONE', *, *, #3500, .T. ) ;
#18860=EDGE_CURVE ( 'NONE', #13663, #38278, #9788, .T. ) ;
#18866=MANIFOLD_SOLID_BREP ( 'Chamfer1', #19442 ) ;
#18869=CARTESIAN_POINT ( 'NONE',  ( 0.05999999999999990757, -0.03575622569115821658, -0.1978615321325044307 ) ) ;
#18928=ORIENTED_EDGE ( 'NONE', *, *, #4363, .F. ) ;
#18955=DIRECTION ( 'NONE',  ( -1.000000000000000000, -7.857794173099924470E-32, -8.628166150854818811E-32 ) ) ;
#18958=SHAPE_REPRESENTATION_RELATIONSHIP ( 'NONE' , 'NONE' ,  #7794, #14212 ) ;
#18974=ORIENTED_EDGE ( 'NONE', *, *, #20091, .F. ) ;
#18976=VERTEX_POINT ( 'NONE', #4011 ) ;
#18981=LINE ( 'NONE', #15888, #15409 ) ;
#19031=LINE ( 'NONE', #36588, #26404 ) ;
#19079=ORIENTED_EDGE ( 'NONE', *, *, #26296, .T. ) ;
#19102=FACE_OUTER_BOUND ( 'NONE', #57, .T. ) ;
#19122=ORIENTED_EDGE ( 'NONE', *, *, #27569, .T. ) ;
#19127=AXIS2_PLACEMENT_3D ( 'NONE', #6203, #18555, #31112 ) ;
#19141=DIRECTION ( 'NONE',  ( -0.4999999999999998890, -0.7377595849475270251, -0.4535535192433776119 ) ) ;
#19162=DIRECTION ( 'NONE',  ( 0.000000000000000000, 0.000000000000000000, 1.000000000000000000 ) ) ;
#19222=ORIENTED_EDGE ( 'NONE', *, *, #19530, .T. ) ;
#19233=DIRECTION ( 'NONE',  ( -1.000000000000000000, -7.857794173099924470E-32, -8.628166150854818811E-32 ) ) ;
#19241=AXIS2_PLACEMENT_3D ( 'NONE', #22831, #25690, #19708 ) ;
#19342=AXIS2_PLACEMENT_3D ( 'NONE', #8965, #37154, #11841 ) ;
#19351=ADVANCED_FACE ( 'NONE', ( #33505 ), #5746, .F. ) ;
#19389=DIRECTION ( 'NONE',  ( -6.162975822039154730E-33, 0.000000000000000000, -1.000000000000000000 ) ) ;
#19405=CIRCLE ( 'NONE', #24663, 0.5614999999999926716 ) ;
#19442=CLOSED_SHELL ( 'NONE', ( #21480, #18269, #24090, #18545, #21599, #30577, #7361, #22740, #29500, #24537, #16275, #21291, #1163, #4379, #9668, #39565, #5986, #32119, #32553, #34209, #29961, #33536, #37064, #37583, #4131, #8274, #2893, #5932, #33641, #35130, #26892, #38972, #21260, #17681, #14917, #38147, #19351, #23053, #35935, #14906, #16591, #2391, #5833, #5608, #18487, #28869, #37621, #33404, #18028, #14167, #9681 ) ) ;
#19444=ORIENTED_EDGE ( 'NONE', *, *, #29769, .F. ) ;
#19462=CARTESIAN_POINT ( 'NONE',  ( 0.03113248654051816583, 0.1919340784543128453, -0.1767348310837237868 ) ) ;
#19503=ORIENTED_EDGE ( 'NONE', *, *, #26093, .F. ) ;
#19525=DIRECTION ( 'NONE',  ( 0.8660254037844390407, 0.3322823180458172043, -0.3736153919662543732 ) ) ;
#19530=EDGE_CURVE ( 'NONE', #38515, #14658, #31460, .T. ) ;
#19533=AXIS2_PLACEMENT_3D ( 'NONE', #13601, #3527, #6799 ) ;
#19542=DIRECTION ( 'NONE',  ( 0.000000000000000000, 0.000000000000000000, 1.000000000000000000 ) ) ;
#19551=EDGE_CURVE ( 'NONE', #37239, #6091, #12711, .T. ) ;
#19593=DIRECTION ( 'NONE',  ( -6.162975822039149256E-32, 0.5237184928541296358, -0.8518913899333639961 ) ) ;
#19607=LINE ( 'NONE', #7221, #12638 ) ;
#19648=EDGE_CURVE ( 'NONE', #14789, #23080, #7147, .T. ) ;
#19670=CARTESIAN_POINT ( 'NONE',  ( 0.000000000000000000, 0.3931478764542372661, 0.2416960844521746365 ) ) ;
#19687=EDGE_CURVE ( 'NONE', #35558, #21667, #4157, .T. ) ;
#19708=DIRECTION ( 'NONE',  ( 0.000000000000000000, 0.000000000000000000, -1.000000000000000000 ) ) ;
#19741=DIRECTION ( 'NONE',  ( 1.000000000000000000, 6.779273404243070203E-32, 4.314083075427408311E-32 ) ) ;
#19783=EDGE_CURVE ( 'NONE', #14101, #37863, #30451, .T. ) ;
#19790=CONICAL_SURFACE ( 'NONE', #11888, 0.1500000000000009936, 1.047197551196599630 ) ;
#19815=AXIS2_PLACEMENT_3D ( 'NONE', #22260, #22452, #24731 ) ;
#19874=VECTOR ( 'NONE', #36379, 39.37007874015748143 ) ;
#19878=DIRECTION ( 'NONE',  ( 0.000000000000000000, 0.000000000000000000, -1.000000000000000000 ) ) ;
#19896=ORIENTED_EDGE ( 'NONE', *, *, #14000, .T. ) ;
#19902=PLANE ( 'NONE',  #39093 ) ;
#19924=ORIENTED_EDGE ( 'NONE', *, *, #26296, .F. ) ;
#19927=LINE ( 'NONE', #3693, #16501 ) ;
#19945=ORIENTED_EDGE ( 'NONE', *, *, #34783, .T. ) ;
#19988=ORIENTED_EDGE ( 'NONE', *, *, #33172, .T. ) ;
#20029=EDGE_CURVE ( 'NONE', #39766, #6871, #2356, .T. ) ;
#20031=ORIENTED_EDGE ( 'NONE', *, *, #24794, .F. ) ;
#20078=DIRECTION ( 'NONE',  ( -1.000000000000000000, -7.857794173099924470E-32, -8.628166150854818811E-32 ) ) ;
#20085=ORIENTED_EDGE ( 'NONE', *, *, #33172, .F. ) ;
#20091=EDGE_CURVE ( 'NONE', #10562, #18074, #12009, .T. ) ;
#20188=VERTEX_POINT ( 'NONE', #25388 ) ;
#20296=DIRECTION ( 'NONE',  ( 4.930380657631323784E-32, 0.7472307839325098566, 0.6645646360916346307 ) ) ;
#20310=VERTEX_POINT ( 'NONE', #2484 ) ;
#20334=EDGE_CURVE ( 'NONE', #5233, #1162, #9451, .T. ) ;
#20397=CARTESIAN_POINT ( 'NONE',  ( 0.000000000000000000, 0.1428018198284763673, -0.2638325989215043466 ) ) ;
#20401=ORIENTED_EDGE ( 'NONE', *, *, #39307, .F. ) ;
#20504=FACE_OUTER_BOUND ( 'NONE', #38607, .T. ) ;
#20515=PRODUCT_DEFINITION ( 'UNKNOWN', '', #22018, #12057 ) ;
#20543=CARTESIAN_POINT ( 'NONE',  ( 0.05999999999999990757, -0.1960639381401260983, -0.03948331496955496261 ) ) ;
#20588=EDGE_LOOP ( 'NONE', ( #38844, #13303, #18396, #8385 ) ) ;
#20623=EDGE_CURVE ( 'NONE', #20310, #15679, #37697, .T. ) ;
#20640=ORIENTED_EDGE ( 'NONE', *, *, #37112, .F. ) ;
#20652=VECTOR ( 'NONE', #28314, 39.37007874015748143 ) ;
#20667=AXIS2_PLACEMENT_3D ( 'NONE', #815, #6532, #26 ) ;
#20681=DIRECTION ( 'NONE',  ( -6.162975822039154730E-33, 0.000000000000000000, -1.000000000000000000 ) ) ;
#20717=FACE_BOUND ( 'NONE', #1950, .T. ) ;
#20738=EDGE_CURVE ( 'NONE', #37734, #1197, #4185, .T. ) ;
#20769=CARTESIAN_POINT ( 'NONE',  ( 0.000000000000000000, 0.7171888913565960255, -0.2950238883388468514 ) ) ;
#20789=SHAPE_DEFINITION_REPRESENTATION ( #20890, #7794 ) ;
#20792=EDGE_CURVE ( 'NONE', #24668, #37734, #28508, .T. ) ;
#20799=CIRCLE ( 'NONE', #6975, 0.06250000000000001388 ) ;
#20870=ORIENTED_EDGE ( 'NONE', *, *, #3207, .F. ) ;
#20876=CARTESIAN_POINT ( 'NONE',  ( 0.03113248654051816583, -0.3829990175980249600, -0.3390339253215535198 ) ) ;
#20890=PRODUCT_DEFINITION_SHAPE ( 'NONE', 'NONE',  #20515 ) ;
#20914=ORIENTED_EDGE ( 'NONE', *, *, #29852, .T. ) ;
#20947=LINE ( 'NONE', #24236, #10591 ) ;
#20959=VERTEX_POINT ( 'NONE', #3643 ) ;
#21073=EDGE_CURVE ( 'NONE', #22141, #37239, #16807, .T. ) ;
#21083=CARTESIAN_POINT ( 'NONE',  ( 0.05999999999999990757, 0.1428018198284763673, -0.2638325989215043466 ) ) ;
#21108=DIRECTION ( 'NONE',  ( 0.000000000000000000, 0.000000000000000000, -1.000000000000000000 ) ) ;
#21141=AXIS2_PLACEMENT_3D ( 'NONE', #17611, #4244, #7527 ) ;
#21229=FACE_OUTER_BOUND ( 'NONE', #15264, .T. ) ;
#21233=EDGE_CURVE ( 'NONE', #22334, #26563, #32460, .T. ) ;
#21242=EDGE_CURVE ( 'NONE', #23685, #24060, #26682, .T. ) ;
#21249=ORIENTED_EDGE ( 'NONE', *, *, #19783, .F. ) ;
#21260=ADVANCED_FACE ( 'NONE', ( #35924 ), #16997, .F. ) ;
#21280=VECTOR ( 'NONE', #40421, 39.37007874015748143 ) ;
#21289=DIRECTION ( 'NONE',  ( -1.000000000000000000, -7.857794173099924470E-32, -8.628166150854818811E-32 ) ) ;
#21291=ADVANCED_FACE ( 'NONE', ( #13890, #26464, #39000, #39216 ), #36925, .T. ) ;
#21309=AXIS2_PLACEMENT_3D ( 'NONE', #35390, #25953, #3515 ) ;
#21324=CARTESIAN_POINT ( 'NONE',  ( 0.000000000000000000, 0.6410130462957083219, -0.4300623794142590661 ) ) ;
#21367=LINE ( 'NONE', #30609, #8584 ) ;
#21375=ORIENTED_EDGE ( 'NONE', *, *, #30362, .F. ) ;
#21385=CARTESIAN_POINT ( 'NONE',  ( 0.000000000000000000, 0.000000000000000000, 0.000000000000000000 ) ) ;
#21417=ORIENTED_EDGE ( 'NONE', *, *, #14000, .F. ) ;
#21418=CARTESIAN_POINT ( 'NONE',  ( 0.03113248654051816583, 0.000000000000000000, 0.000000000000000000 ) ) ;
#21427=DIRECTION ( 'NONE',  ( -1.000000000000000000, -7.857794173099924470E-32, -8.628166150854818811E-32 ) ) ;
#21438=EDGE_LOOP ( 'NONE', ( #3746, #10617, #31566, #37798 ) ) ;
#21452=DIRECTION ( 'NONE',  ( 0.000000000000000000, 0.000000000000000000, 1.000000000000000000 ) ) ;
#21480=ADVANCED_FACE ( 'NONE', ( #6264 ), #13445, .T. ) ;
#21513=DIRECTION ( 'NONE',  ( 0.000000000000000000, 0.000000000000000000, 1.000000000000000000 ) ) ;
#21599=ADVANCED_FACE ( 'NONE', ( #26576 ), #26784, .F. ) ;
#21667=VERTEX_POINT ( 'NONE', #23040 ) ;
#21698=ORIENTED_EDGE ( 'NONE', *, *, #37112, .T. ) ;
#21724=DIRECTION ( 'NONE',  ( -0.4999999999999987232, 0.4254978411528142490, 0.7542887956043731190 ) ) ;
#21728=CARTESIAN_POINT ( 'NONE',  ( 0.05999999999999990757, -0.3767386922704979990, -0.2665524483967541269 ) ) ;
#21738=FACE_OUTER_BOUND ( 'NONE', #31631, .T. ) ;
#21789=FACE_OUTER_BOUND ( 'NONE', #24290, .T. ) ;
#21927=ORIENTED_EDGE ( 'NONE', *, *, #5363, .T. ) ;
#21947=DIRECTION ( 'NONE',  ( 0.000000000000000000, -0.6645646360916347417, 0.7472307839325098566 ) ) ;
#21951=AXIS2_PLACEMENT_3D ( 'NONE', #36365, #23455, #17248 ) ;
#21970=LINE ( 'NONE', #3043, #307 ) ;
#22011=AXIS2_PLACEMENT_3D ( 'NONE', #3013, #36740, #39835 ) ;
#22015=VECTOR ( 'NONE', #17071, 39.37007874015748143 ) ;
#22018=PRODUCT_DEFINITION_FORMATION_WITH_SPECIFIED_SOURCE ( 'ANY', '', #27114, .NOT_KNOWN. ) ;
#22029=CARTESIAN_POINT ( 'NONE',  ( 0.03113248654051816583, -0.3165425539888620521, -0.4137570037148034507 ) ) ;
#22055=CARTESIAN_POINT ( 'NONE',  ( 0.03113248654051816583, -0.4415087982045245996, -0.1343585914930097158 ) ) ;
#22059=CONICAL_SURFACE ( 'NONE', #14810, 0.1500000000000011324, 1.047197551196599630 ) ;
#22071=AXIS2_PLACEMENT_3D ( 'NONE', #26050, #13274, #22953 ) ;
#22124=ORIENTED_EDGE ( 'NONE', *, *, #18860, .F. ) ;
#22141=VERTEX_POINT ( 'NONE', #8960 ) ;
#22142=CARTESIAN_POINT ( 'NONE',  ( 0.05999999999999990757, 0.7171888913565960255, -0.2950238883388468514 ) ) ;
#22174=FACE_OUTER_BOUND ( 'NONE', #5105, .T. ) ;
#22260=CARTESIAN_POINT ( 'NONE',  ( 0.05999999999999990757, 0.1428018198284763673, -0.2638325989215043466 ) ) ;
#22261=DIRECTION ( 'NONE',  ( 1.000000000000000000, 6.779273404243070203E-32, 4.314083075427408311E-32 ) ) ;
#22308=CARTESIAN_POINT ( 'NONE',  ( 0.05999999999999990757, 0.1369749717427355129, -0.1457321416712075435 ) ) ;
#22313=CARTESIAN_POINT ( 'NONE',  ( 0.05999999999999990757, 0.7171888913565960255, -0.2950238883388468514 ) ) ;
#22318=CARTESIAN_POINT ( 'NONE',  ( 0.05999999999999990757, 0.7171888913565960255, -0.2950238883388468514 ) ) ;
#22327=DIRECTION ( 'NONE',  ( -1.000000000000000000, -6.779273404243070203E-32, -4.314083075427408311E-32 ) ) ;
#22334=VERTEX_POINT ( 'NONE', #37093 ) ;
#22362=ORIENTED_EDGE ( 'NONE', *, *, #22787, .F. ) ;
#22389=VERTEX_POINT ( 'NONE', #25570 ) ;
#22409=FACE_OUTER_BOUND ( 'NONE', #18738, .T. ) ;
#22436=LINE ( 'NONE', #25519, #39078 ) ;
#22449=VECTOR ( 'NONE', #25479, 39.37007874015748143 ) ;
#22452=DIRECTION ( 'NONE',  ( -1.000000000000000000, -6.779273404243070203E-32, -4.314083075427408311E-32 ) ) ;
#22456=VECTOR ( 'NONE', #11055, 39.37007874015748143 ) ;
#22513=EDGE_CURVE ( 'NONE', #24668, #5937, #16715, .T. ) ;
#22545=AXIS2_PLACEMENT_3D ( 'NONE', #9242, #21427, #15222 ) ;
#22551=LINE ( 'NONE', #32186, #17910 ) ;
#22578=VECTOR ( 'NONE', #12010, 39.37007874015748854 ) ;
#22590=ORIENTED_EDGE ( 'NONE', *, *, #20029, .T. ) ;
#22600=EDGE_LOOP ( 'NONE', ( #25991, #28495, #11225, #21249 ) ) ;
#22626=AXIS2_PLACEMENT_3D ( 'NONE', #10010, #13298, #19878 ) ;
#22650=DIRECTION ( 'NONE',  ( -1.000000000000000000, -7.857794173099924470E-32, -8.628166150854818811E-32 ) ) ;
#22667=VECTOR ( 'NONE', #20296, 39.37007874015748143 ) ;
#22740=ADVANCED_FACE ( 'NONE', ( #14130 ), #1813, .F. ) ;
#22784=AXIS2_PLACEMENT_3D ( 'NONE', #31750, #3567, #542 ) ;
#22787=EDGE_CURVE ( 'NONE', #30962, #39909, #6643, .T. ) ;
#22792=EDGE_CURVE ( 'NONE', #31508, #18074, #13214, .T. ) ;
#22800=EDGE_CURVE ( 'NONE', #30067, #3878, #4639, .T. ) ;
#22807=ORIENTED_EDGE ( 'NONE', *, *, #10168, .T. ) ;
#22831=CARTESIAN_POINT ( 'NONE',  ( 0.05999999999999990757, -0.3458405862425447119, -0.1052451372150005060 ) ) ;
#22864=CARTESIAN_POINT ( 'NONE',  ( 0.05999999999999990757, 0.000000000000000000, 0.000000000000000000 ) ) ;
#22953=DIRECTION ( 'NONE',  ( 0.000000000000000000, 0.000000000000000000, 1.000000000000000000 ) ) ;
#22965=DIRECTION ( 'NONE',  ( -1.000000000000000000, -7.857794173099924470E-32, -8.628166150854818811E-32 ) ) ;
#22969=ORIENTED_EDGE ( 'NONE', *, *, #4622, .T. ) ;
#23040=CARTESIAN_POINT ( 'NONE',  ( 0.03113248654051816583, 0.1428018198284763673, -0.1638325989215043410 ) ) ;
#23043=CARTESIAN_POINT ( 'NONE',  ( 0.05999999999999990757, 0.6410130462957083219, -0.4300623794142590661 ) ) ;
#23053=ADVANCED_FACE ( 'NONE', ( #28426 ), #772, .F. ) ;
#23061=EDGE_CURVE ( 'NONE', #35558, #553, #2930, .T. ) ;
#23076=LINE ( 'NONE', #25552, #10537 ) ;
#23080=VERTEX_POINT ( 'NONE', #37468 ) ;
#23108=CARTESIAN_POINT ( 'NONE',  ( -1.990949339309697573E-32, -3.491513147198971704E-33, 0.4614999999999880864 ) ) ;
#23112=( NAMED_UNIT ( * ) SI_UNIT ( $, .STERADIAN. ) SOLID_ANGLE_UNIT ( ) );
#23156=AXIS2_PLACEMENT_3D ( 'NONE', #17484, #2466, #33104 ) ;
#23160=DIRECTION ( 'NONE',  ( -1.000000000000000000, -6.779273404243070203E-32, -4.314083075427407763E-32 ) ) ;
#23245=EDGE_CURVE ( 'NONE', #31435, #22141, #29663, .T. ) ;
#23254=ORIENTED_EDGE ( 'NONE', *, *, #5688, .F. ) ;
#23268=CARTESIAN_POINT ( 'NONE',  ( 0.05999999999999990757, -0.1022126893003200560, -0.2231384537392532841 ) ) ;
#23313=CARTESIAN_POINT ( 'NONE',  ( 0.05999999999999990757, 0.01983442501260774746, 0.03516089415102874316 ) ) ;
#23326=DIRECTION ( 'NONE',  ( 0.000000000000000000, 1.821231995776163252E-15, -1.000000000000000000 ) ) ;
#23351=ORIENTED_EDGE ( 'NONE', *, *, #31320, .T. ) ;
#23398=DIMENSIONAL_EXPONENTS ( 1.000000000000000000, 0.000000000000000000, 0.000000000000000000, 0.000000000000000000, 0.000000000000000000, 0.000000000000000000, 0.000000000000000000 ) ;
#23405=CARTESIAN_POINT ( 'NONE',  ( 0.05999999999999990757, 0.1997995745459845707, -0.008951536808938237097 ) ) ;
#23431=CIRCLE ( 'NONE', #16831, 0.1500000000000009936 ) ;
#23455=DIRECTION ( 'NONE',  ( -1.000000000000000000, -6.779273404243070203E-32, -4.314083075427408311E-32 ) ) ;
#23458=VECTOR ( 'NONE', #28514, 39.37007874015748143 ) ;
#23576=DIRECTION ( 'NONE',  ( 0.8660254037844391517, 0.4259456949666812209, 0.2618592464270645404 ) ) ;
#23584=CARTESIAN_POINT ( 'NONE',  ( 0.03113248654051816583, 0.7171888913565960255, -0.2950238883388468514 ) ) ;
#23593=DIRECTION ( 'NONE',  ( 2.157041537713701966E-32, -0.8709776783778060416, 0.4913225862583635584 ) ) ;
#23595=CARTESIAN_POINT ( 'NONE',  ( 0.05999999999999990757, -0.3458405862425447119, -0.1052451372150005060 ) ) ;
#23647=VERTEX_POINT ( 'NONE', #18553 ) ;
#23665=LINE ( 'NONE', #16883, #5533 ) ;
#23685=VERTEX_POINT ( 'NONE', #36855 ) ;
#23735=EDGE_CURVE ( 'NONE', #5937, #24586, #18149, .T. ) ;
#23797=VECTOR ( 'NONE', #663, 39.37007874015748143 ) ;
#23856=CARTESIAN_POINT ( 'NONE',  ( 0.05999999999999990757, 0.2463462108298974940, -0.03520871226632921180 ) ) ;
#23889=ORIENTED_EDGE ( 'NONE', *, *, #22800, .T. ) ;
#23893=ORIENTED_EDGE ( 'NONE', *, *, #6693, .F. ) ;
#23894=VECTOR ( 'NONE', #14295, 39.37007874015748143 ) ;
#23926=AXIS2_PLACEMENT_3D ( 'NONE', #31992, #12648, #34669 ) ;
#23943=ORIENTED_EDGE ( 'NONE', *, *, #27361, .F. ) ;
#23987=AXIS2_PLACEMENT_3D ( 'NONE', #40449, #31201, #34475 ) ;
#24012=EDGE_CURVE ( 'NONE', #5937, #10562, #39424, .T. ) ;
#24060=VERTEX_POINT ( 'NONE', #8620 ) ;
#24080=FACE_OUTER_BOUND ( 'NONE', #4440, .T. ) ;
#24090=ADVANCED_FACE ( 'NONE', ( #27979 ), #3302, .F. ) ;
#24096=ORIENTED_EDGE ( 'NONE', *, *, #32928, .F. ) ;
#24116=LINE ( 'NONE', #17516, #25079 ) ;
#24125=DIRECTION ( 'NONE',  ( 1.000000000000000000, 6.779273404243070203E-32, 4.314083075427408311E-32 ) ) ;
#24157=ORIENTED_EDGE ( 'NONE', *, *, #3500, .F. ) ;
#24183=FACE_OUTER_BOUND ( 'NONE', #8345, .T. ) ;
#24236=CARTESIAN_POINT ( 'NONE',  ( 0.05999999999999990757, 0.4783370154475735103, 0.2940679337375869395 ) ) ;
#24247=DIRECTION ( 'NONE',  ( 0.000000000000000000, 0.000000000000000000, -1.000000000000000000 ) ) ;
#24263=EDGE_CURVE ( 'NONE', #1197, #29289, #31873, .T. ) ;
#24290=EDGE_LOOP ( 'NONE', ( #9866, #10288, #6518, #24804 ) ) ;
#24335=ORIENTED_EDGE ( 'NONE', *, *, #5096, .F. ) ;
#24382=CARTESIAN_POINT ( 'NONE',  ( 0.05999999999999990757, 0.5386841146467193919, -0.2575246450067292248 ) ) ;
#24398=CARTESIAN_POINT ( 'NONE',  ( 0.05999999999999990757, -0.1944112117964420239, -0.1713095900442092034 ) ) ;
#24416=AXIS2_PLACEMENT_3D ( 'NONE', #17016, #5063, #35942 ) ;
#24445=VERTEX_POINT ( 'NONE', #19670 ) ;
#24503=AXIS2_PLACEMENT_3D ( 'NONE', #4490, #29597, #10890 ) ;
#24537=ADVANCED_FACE ( 'NONE', ( #14103 ), #36107, .T. ) ;
#24552=CARTESIAN_POINT ( 'NONE',  ( 0.05999999999999990757, -0.4893429041855150707, -0.1489153186320146816 ) ) ;
#24574=DIRECTION ( 'NONE',  ( -6.162975822039154046E-33, 0.000000000000000000, -1.000000000000000000 ) ) ;
#24578=DIRECTION ( 'NONE',  ( 0.000000000000000000, 0.000000000000000000, 1.000000000000000000 ) ) ;
#24581=DIRECTION ( 'NONE',  ( -1.000000000000000000, -7.857794173099924470E-32, -8.628166150854818811E-32 ) ) ;
#24586=VERTEX_POINT ( 'NONE', #32412 ) ;
#24625=AXIS2_PLACEMENT_3D ( 'NONE', #15577, #5880, #12288 ) ;
#24663=AXIS2_PLACEMENT_3D ( 'NONE', #37970, #7444, #37764 ) ;
#24668=VERTEX_POINT ( 'NONE', #37326 ) ;
#24731=DIRECTION ( 'NONE',  ( 0.000000000000000000, 1.821231995776161674E-15, -1.000000000000000000 ) ) ;
#24743=CIRCLE ( 'NONE', #5014, 0.06250000000000001388 ) ;
#24786=DIRECTION ( 'NONE',  ( 0.000000000000000000, 0.000000000000000000, 1.000000000000000000 ) ) ;
#24794=EDGE_CURVE ( 'NONE', #38515, #7881, #25695, .T. ) ;
#24804=ORIENTED_EDGE ( 'NONE', *, *, #26651, .F. ) ;
#24821=CARTESIAN_POINT ( 'NONE',  ( 0.05999999999999990757, -0.02383748379410547888, -0.1985743547550029575 ) ) ;
#24840=DIRECTION ( 'NONE',  ( -1.000000000000000000, -7.857794173099924470E-32, -8.628166150854818811E-32 ) ) ;
#24877=CARTESIAN_POINT ( 'NONE',  ( 0.05999999999999990757, -0.2940959072101921867, -0.05922497245433272495 ) ) ;
#24903=CARTESIAN_POINT ( 'NONE',  ( 0.03113248654051816583, 0.6304109427692223822, -0.1442409525262416947 ) ) ;
#24907=ORIENTED_EDGE ( 'NONE', *, *, #39307, .T. ) ;
#24967=FACE_OUTER_BOUND ( 'NONE', #40144, .T. ) ;
#24984=DIRECTION ( 'NONE',  ( 0.000000000000000000, 0.000000000000000000, -1.000000000000000000 ) ) ;
#25015=VECTOR ( 'NONE', #35970, 39.37007874015748143 ) ;
#25065=DIRECTION ( 'NONE',  ( -1.000000000000000000, -7.857794173099924470E-32, -8.628166150854818811E-32 ) ) ;
#25079=VECTOR ( 'NONE', #30468, 39.37007874015748854 ) ;
#25088=CARTESIAN_POINT ( 'NONE',  ( 0.03113248654051816583, 0.5878163732725504298, -0.1704268771689479434 ) ) ;
#25089=VERTEX_POINT ( 'NONE', #24552 ) ;
#25108=EDGE_LOOP ( 'NONE', ( #40316, #39616, #12107, #38891 ) ) ;
#25122=DIRECTION ( 'NONE',  ( 1.000000000000000000, 6.779273404243070203E-32, 4.314083075427408311E-32 ) ) ;
#25145=EDGE_LOOP ( 'NONE', ( #847, #3316, #28972, #10238 ) ) ;
#25162=VECTOR ( 'NONE', #18955, 39.37007874015748143 ) ;
#25165=CARTESIAN_POINT ( 'NONE',  ( 0.000000000000000000, -0.2940959072101921867, -0.05922497245433272495 ) ) ;
#25179=CARTESIAN_POINT ( 'NONE',  ( -2.638061800623833890E-32, -3.491513147198974441E-33, 0.6114999999999938263 ) ) ;
#25181=EDGE_LOOP ( 'NONE', ( #8800, #6449, #17653, #4144 ) ) ;
#25228=CARTESIAN_POINT ( 'NONE',  ( 0.05999999999999990757, -0.3829990175980249600, -0.3390339253215535198 ) ) ;
#25250=ORIENTED_EDGE ( 'NONE', *, *, #39388, .F. ) ;
#25257=VECTOR ( 'NONE', #7917, 39.37007874015748854 ) ;
#25322=ORIENTED_EDGE ( 'NONE', *, *, #3045, .F. ) ;
#25340=( LENGTH_UNIT ( ) NAMED_UNIT ( * ) SI_UNIT ( $, .METRE. ) );
#25356=DIRECTION ( 'NONE',  ( 0.4999999999999982792, 0.8489817559768471078, 0.1709677689462869299 ) ) ;
#25366=ORIENTED_EDGE ( 'NONE', *, *, #32928, .T. ) ;
#25385=ORIENTED_EDGE ( 'NONE', *, *, #31048, .F. ) ;
#25388=CARTESIAN_POINT ( 'NONE',  ( 0.05999999999999990757, -0.01787811284557883421, -0.1489307660662511357 ) ) ;
#25479=DIRECTION ( 'NONE',  ( -0.4999999999999988898, -0.7377595849475285794, -0.4535535192433760576 ) ) ;
#25514=ORIENTED_EDGE ( 'NONE', *, *, #6126, .F. ) ;
#25519=CARTESIAN_POINT ( 'NONE',  ( 0.05999999999999990757, 0.1428018198284763673, -0.1638325989215043410 ) ) ;
#25552=CARTESIAN_POINT ( 'NONE',  ( 0.000000000000000000, -0.3767386922704979990, -0.2665524483967541269 ) ) ;
#25570=CARTESIAN_POINT ( 'NONE',  ( 0.000000000000000000, 0.2463462108298974940, -0.03520871226632921180 ) ) ;
#25670=CYLINDRICAL_SURFACE ( 'NONE', #10971, 0.2000000000000000389 ) ;
#25690=DIRECTION ( 'NONE',  ( 1.000000000000000000, 6.779273404243070203E-32, 4.314083075427408311E-32 ) ) ;
#25695=CIRCLE ( 'NONE', #37477, 0.1000000000000000194 ) ;
#25725=DIRECTION ( 'NONE',  ( -4.930380657631319405E-32, 0.5237184928541299689, -0.8518913899333638851 ) ) ;
#25759=ORIENTED_EDGE ( 'NONE', *, *, #24263, .T. ) ;
#25772=CARTESIAN_POINT ( 'NONE',  ( 0.05999999999999990757, 0.1428018198284763673, -0.2638325989215043466 ) ) ;
#25802=EDGE_CURVE ( 'NONE', #38544, #23685, #18518, .T. ) ;
#25862=CIRCLE ( 'NONE', #37676, 0.04999999999999994726 ) ;
#25940=LINE ( 'NONE', #23043, #23797 ) ;
#25953=DIRECTION ( 'NONE',  ( 1.000000000000000000, 6.779273404243070203E-32, 4.314083075427408311E-32 ) ) ;
#25961=AXIS2_PLACEMENT_3D ( 'NONE', #13587, #34977, #10088 ) ;
#25991=ORIENTED_EDGE ( 'NONE', *, *, #14966, .T. ) ;
#26024=EDGE_LOOP ( 'NONE', ( #8543, #19079, #28039, #2836 ) ) ;
#26050=CARTESIAN_POINT ( 'NONE',  ( 0.05999999999999990757, 0.000000000000000000, 0.000000000000000000 ) ) ;
#26068=CIRCLE ( 'NONE', #12254, 0.2000000000000000111 ) ;
#26093=EDGE_CURVE ( 'NONE', #24586, #13712, #6021, .T. ) ;
#26137=ORIENTED_EDGE ( 'NONE', *, *, #34843, .T. ) ;
#26156=EDGE_CURVE ( 'NONE', #892, #5233, #29026, .T. ) ;
#26182=AXIS2_PLACEMENT_3D ( 'NONE', #33248, #11231, #27683 ) ;
#26191=LINE ( 'NONE', #10536, #10035 ) ;
#26195=( NAMED_UNIT ( * ) PLANE_ANGLE_UNIT ( ) SI_UNIT ( $, .RADIAN. ) );
#26296=EDGE_CURVE ( 'NONE', #17043, #8681, #15229, .T. ) ;
#26392=DIRECTION ( 'NONE',  ( -1.000000000000000000, -6.779273404243070203E-32, -4.314083075427408311E-32 ) ) ;
#26404=VECTOR ( 'NONE', #19233, 39.37007874015748143 ) ;
#26419=ORIENTED_EDGE ( 'NONE', *, *, #6693, .T. ) ;
#26432=DIRECTION ( 'NONE',  ( 0.000000000000000000, 0.000000000000000000, -1.000000000000000000 ) ) ;
#26438=CARTESIAN_POINT ( 'NONE',  ( 0.05999999999999990757, -0.3165425539888620521, -0.4137570037148034507 ) ) ;
#26464=FACE_OUTER_BOUND ( 'NONE', #5329, .T. ) ;
#26489=VECTOR ( 'NONE', #18493, 39.37007874015748854 ) ;
#26514=LINE ( 'NONE', #20543, #25015 ) ;
#26536=EDGE_CURVE ( 'NONE', #22389, #11737, #6178, .T. ) ;
#26563=VERTEX_POINT ( 'NONE', #22055 ) ;
#26576=FACE_OUTER_BOUND ( 'NONE', #32686, .T. ) ;
#26583=ORIENTED_EDGE ( 'NONE', *, *, #4622, .F. ) ;
#26624=CARTESIAN_POINT ( 'NONE',  ( 0.03113248654051816583, 0.5209315849442416324, 0.3202538583802939098 ) ) ;
#26651=EDGE_CURVE ( 'NONE', #40017, #18976, #29213, .T. ) ;
#26677=CARTESIAN_POINT ( 'NONE',  ( 0.05999999999999990757, 0.000000000000000000, 0.000000000000000000 ) ) ;
#26682=LINE ( 'NONE', #27068, #22667 ) ;
#26700=DIRECTION ( 'NONE',  ( 0.000000000000000000, 0.000000000000000000, -1.000000000000000000 ) ) ;
#26712=CARTESIAN_POINT ( 'NONE',  ( 0.000000000000000000, -0.1022126893003200560, -0.2231384537392532841 ) ) ;
#26727=DIRECTION ( 'NONE',  ( 0.000000000000000000, 0.000000000000000000, 1.000000000000000000 ) ) ;
#26759=DIRECTION ( 'NONE',  ( -1.000000000000000000, -6.779273404243070203E-32, -4.314083075427408311E-32 ) ) ;
#26774=VERTEX_POINT ( 'NONE', #36600 ) ;
#26784=CYLINDRICAL_SURFACE ( 'NONE', #30541, 0.1000000000000000194 ) ;
#26866=ORIENTED_EDGE ( 'NONE', *, *, #31034, .T. ) ;
#26881=PLANE ( 'NONE',  #26182 ) ;
#26890=DIRECTION ( 'NONE',  ( 0.000000000000000000, 0.000000000000000000, 1.000000000000000000 ) ) ;
#26892=ADVANCED_FACE ( 'NONE', ( #34112 ), #21, .F. ) ;
#26899=CARTESIAN_POINT ( 'NONE',  ( 0.03113248654051816583, -0.3458405862425447119, -0.2052451372150005393 ) ) ;
#26923=ORIENTED_EDGE ( 'NONE', *, *, #22800, .F. ) ;
#26984=CARTESIAN_POINT ( 'NONE',  ( 0.000000000000000000, -0.03575622569115821658, -0.2978615321325044363 ) ) ;
#27053=DIRECTION ( 'NONE',  ( -1.000000000000000000, -7.857794173099924470E-32, -8.628166150854818811E-32 ) ) ;
#27068=CARTESIAN_POINT ( 'NONE',  ( 0.05999999999999990757, -0.1354409211049039941, -0.1857769145426272639 ) ) ;
#27114=PRODUCT ( 'Lower cage plate', 'Lower cage plate', '', ( #33499 ) ) ;
#27282=CIRCLE ( 'NONE', #6878, 0.1000000000000000194 ) ;
#27318=AXIS2_PLACEMENT_3D ( 'NONE', #21728, #21947, #36949 ) ;
#27361=EDGE_CURVE ( 'NONE', #31508, #16113, #6285, .T. ) ;
#27408=CARTESIAN_POINT ( 'NONE',  ( 0.03113248654051816583, 0.1969856463038233696, 0.03459270371430114843 ) ) ;
#27427=VERTEX_POINT ( 'NONE', #23108 ) ;
#27458=DIRECTION ( 'NONE',  ( 0.000000000000000000, 0.000000000000000000, 1.000000000000000000 ) ) ;
#27463=CYLINDRICAL_SURFACE ( 'NONE', #35893, 0.1000000000000000056 ) ;
#27481=DIRECTION ( 'NONE',  ( 0.000000000000000000, 0.000000000000000000, -1.000000000000000000 ) ) ;
#27547=CARTESIAN_POINT ( 'NONE',  ( 0.05999999999999990757, 0.7171888913565960255, -0.2950238883388468514 ) ) ;
#27569=EDGE_CURVE ( 'NONE', #24060, #14824, #26191, .T. ) ;
#27593=CARTESIAN_POINT ( 'NONE',  ( 0.000000000000000000, 0.1997995745459845707, -0.008951536808938304751 ) ) ;
#27631=LINE ( 'NONE', #40161, #29006 ) ;
#27683=DIRECTION ( 'NONE',  ( -6.162975822039154730E-33, 0.000000000000000000, -1.000000000000000000 ) ) ;
#27696=CARTESIAN_POINT ( 'NONE',  ( 0.05999999999999990757, 0.2217800815169825301, -0.07875759618522079619 ) ) ;
#27763=DIRECTION ( 'NONE',  ( -1.000000000000000000, -7.857794173099924470E-32, -8.628166150854818811E-32 ) ) ;
#27780=ORIENTED_EDGE ( 'NONE', *, *, #23061, .T. ) ;
#27819=AXIS2_PLACEMENT_3D ( 'NONE', #8920, #2961, #8315 ) ;
#27865=DIRECTION ( 'NONE',  ( 4.930380657631319405E-32, 0.4913225862583635584, 0.8709776783778060416 ) ) ;
#27876=CONICAL_SURFACE ( 'NONE', #23926, 0.1500000000000009936, 1.047197551196599408 ) ;
#27887=CARTESIAN_POINT ( 'NONE',  ( 0.05999999999999990757, 0.000000000000000000, 0.000000000000000000 ) ) ;
#27899=AXIS2_PLACEMENT_3D ( 'NONE', #29039, #3752, #32130 ) ;
#27925=CIRCLE ( 'NONE', #6236, 0.1000000000000000194 ) ;
#27979=FACE_OUTER_BOUND ( 'NONE', #30405, .T. ) ;
#27981=LINE ( 'NONE', #22029, #7228 ) ;
#27996=CARTESIAN_POINT ( 'NONE',  ( 0.05999999999999990757, 0.4783370154475778957, 0.2940679337375899927 ) ) ;
#27998=ORIENTED_EDGE ( 'NONE', *, *, #8168, .F. ) ;
#28010=CARTESIAN_POINT ( 'NONE',  ( 0.05999999999999990757, 0.5209315849442416324, 0.3202538583802939098 ) ) ;
#28015=( NAMED_UNIT ( * ) PLANE_ANGLE_UNIT ( ) SI_UNIT ( $, .RADIAN. ) );
#28018=EDGE_CURVE ( 'NONE', #21667, #3878, #18605, .T. ) ;
#28021=EDGE_CURVE ( 'NONE', #14789, #37239, #6388, .T. ) ;
#28039=ORIENTED_EDGE ( 'NONE', *, *, #34780, .T. ) ;
#28066=DIRECTION ( 'NONE',  ( 1.000000000000000000, 6.779273404243070203E-32, 4.314083075427408311E-32 ) ) ;
#28151=ORIENTED_EDGE ( 'NONE', *, *, #19687, .F. ) ;
#28296=LINE ( 'NONE', #19462, #31252 ) ;
#28298=AXIS2_PLACEMENT_3D ( 'NONE', #33279, #32864, #26727 ) ;
#28314=DIRECTION ( 'NONE',  ( 0.4999999999999972800, -0.7377595849475294676, -0.4535535192433765017 ) ) ;
#28375=ORIENTED_EDGE ( 'NONE', *, *, #23735, .T. ) ;
#28411=( NAMED_UNIT ( * ) SI_UNIT ( $, .STERADIAN. ) SOLID_ANGLE_UNIT ( ) );
#28421=ORIENTED_EDGE ( 'NONE', *, *, #15243, .T. ) ;
#28426=FACE_OUTER_BOUND ( 'NONE', #6858, .T. ) ;
#28486=ORIENTED_EDGE ( 'NONE', *, *, #5104, .F. ) ;
#28495=ORIENTED_EDGE ( 'NONE', *, *, #20738, .F. ) ;
#28508=CIRCLE ( 'NONE', #4814, 0.1499999999999990785 ) ;
#28514=DIRECTION ( 'NONE',  ( -0.4999999999999981681, 0.5755298573121171435, -0.6471208413753152255 ) ) ;
#28607=ORIENTED_EDGE ( 'NONE', *, *, #28018, .F. ) ;
#28637=CARTESIAN_POINT ( 'NONE',  ( 0.03113248654051816583, -0.1960639381401260983, -0.03948331496955503200 ) ) ;
#28646=CARTESIAN_POINT ( 'NONE',  ( 0.000000000000000000, -0.2276394436010286959, -0.1339480508475833498 ) ) ;
#28695=ORIENTED_EDGE ( 'NONE', *, *, #38860, .T. ) ;
#28711=FACE_OUTER_BOUND ( 'NONE', #22600, .T. ) ;
#28730=ORIENTED_EDGE ( 'NONE', *, *, #5363, .F. ) ;
#28752=VERTEX_POINT ( 'NONE', #12464 ) ;
#28806=CARTESIAN_POINT ( 'NONE',  ( 0.05999999999999990757, 0.2954784694557334168, 0.05188905557145093855 ) ) ;
#28811=EDGE_CURVE ( 'NONE', #20188, #28752, #7898, .T. ) ;
#28820=DIRECTION ( 'NONE',  ( 1.000000000000000000, 6.779273404243070203E-32, 4.314083075427408311E-32 ) ) ;
#28869=ADVANCED_FACE ( 'NONE', ( #5223 ), #17774, .T. ) ;
#28872=ORIENTED_EDGE ( 'NONE', *, *, #8168, .T. ) ;
#28912=AXIS2_PLACEMENT_3D ( 'NONE', #22313, #6642, #21513 ) ;
#28972=ORIENTED_EDGE ( 'NONE', *, *, #32847, .T. ) ;
#28997=DIRECTION ( 'NONE',  ( 0.000000000000000000, 0.000000000000000000, -1.000000000000000000 ) ) ;
#29006=VECTOR ( 'NONE', #40376, 39.37007874015748854 ) ;
#29026=CIRCLE ( 'NONE', #7993, 0.04999999999999994726 ) ;
#29039=CARTESIAN_POINT ( 'NONE',  ( 0.05999999999999990757, 0.1428018198284763673, -0.2638325989215043466 ) ) ;
#29041=CARTESIAN_POINT ( 'NONE',  ( 0.05999999999999990757, -0.3852620677835773555, -0.4748740771268961103 ) ) ;
#29062=CIRCLE ( 'NONE', #5372, 0.1000000000000000056 ) ;
#29072=EDGE_CURVE ( 'NONE', #6871, #199, #32393, .T. ) ;
#29179=DIRECTION ( 'NONE',  ( 0.000000000000000000, 0.000000000000000000, -1.000000000000000000 ) ) ;
#29185=ORIENTED_EDGE ( 'NONE', *, *, #29072, .T. ) ;
#29191=DIRECTION ( 'NONE',  ( -1.000000000000000000, -7.857794173099924470E-32, -8.628166150854818811E-32 ) ) ;
#29213=LINE ( 'NONE', #16459, #3418 ) ;
#29230=EDGE_LOOP ( 'NONE', ( #16648, #39758, #5512, #11440 ) ) ;
#29242=AXIS2_PLACEMENT_3D ( 'NONE', #25165, #15695, #6832 ) ;
#29266=CARTESIAN_POINT ( 'NONE',  ( 0.05999999999999990757, -9.785038312124664947E-34, 0.5614999999999926716 ) ) ;
#29289=VERTEX_POINT ( 'NONE', #34136 ) ;
#29389=CARTESIAN_POINT ( 'NONE',  ( 0.03113248654051816583, 0.1428018198284763673, -0.2638325989215043466 ) ) ;
#29438=ORIENTED_EDGE ( 'NONE', *, *, #17975, .F. ) ;
#29454=PLANE ( 'NONE',  #12588 ) ;
#29483=VERTEX_POINT ( 'NONE', #13743 ) ;
#29500=ADVANCED_FACE ( 'NONE', ( #7352 ), #10665, .F. ) ;
#29526=EDGE_LOOP ( 'NONE', ( #10432, #16791, #23893, #7348 ) ) ;
#29557=CARTESIAN_POINT ( 'NONE',  ( 0.05999999999999990757, 0.2954784694557334168, 0.05188905557145093855 ) ) ;
#29562=CIRCLE ( 'NONE', #17081, 0.06250000000000000000 ) ;
#29597=DIRECTION ( 'NONE',  ( -1.000000000000000000, -6.779273404243070203E-32, -4.314083075427408311E-32 ) ) ;
#29609=EDGE_CURVE ( 'NONE', #39909, #20959, #7970, .T. ) ;
#29614=EDGE_CURVE ( 'NONE', #16113, #29483, #14972, .T. ) ;
#29663=CIRCLE ( 'NONE', #11917, 0.1550424246542357609 ) ;
#29722=ORIENTED_EDGE ( 'NONE', *, *, #10296, .T. ) ;
#29747=VERTEX_POINT ( 'NONE', #9608 ) ;
#29755=ORIENTED_EDGE ( 'NONE', *, *, #37405, .T. ) ;
#29769=EDGE_CURVE ( 'NONE', #9616, #6871, #21970, .T. ) ;
#29814=EDGE_CURVE ( 'NONE', #20188, #38276, #32429, .T. ) ;
#29852=EDGE_CURVE ( 'NONE', #23080, #199, #38384, .T. ) ;
#29881=CARTESIAN_POINT ( 'NONE',  ( 0.000000000000000000, -0.2276394436010286959, -0.1339480508475833498 ) ) ;
#29893=CIRCLE ( 'NONE', #6881, 0.1500000000000009936 ) ;
#29938=CARTESIAN_POINT ( 'NONE',  ( 0.000000000000000000, 0.000000000000000000, 0.000000000000000000 ) ) ;
#29947=ORIENTED_EDGE ( 'NONE', *, *, #26156, .T. ) ;
#29961=ADVANCED_FACE ( 'NONE', ( #36720 ), #5437, .T. ) ;
#29984=AXIS2_PLACEMENT_3D ( 'NONE', #21385, #2840, #5720 ) ;
#29999=ORIENTED_EDGE ( 'NONE', *, *, #36038, .T. ) ;
#30067=VERTEX_POINT ( 'NONE', #15328 ) ;
#30166=ORIENTED_EDGE ( 'NONE', *, *, #6121, .F. ) ;
#30214=DIRECTION ( 'NONE',  ( -1.000000000000000000, -7.857794173099924470E-32, -8.628166150854818811E-32 ) ) ;
#30224=CARTESIAN_POINT ( 'NONE',  ( 0.03113248654051816583, -0.3767386922704979990, -0.2665524483967541269 ) ) ;
#30228=ORIENTED_EDGE ( 'NONE', *, *, #37400, .F. ) ;
#30242=CARTESIAN_POINT ( 'NONE',  ( 0.05999999999999990757, -0.03575622569115821658, -0.2978615321325044363 ) ) ;
#30295=ORIENTED_EDGE ( 'NONE', *, *, #31088, .F. ) ;
#30326=CONICAL_SURFACE ( 'NONE', #7339, 0.1500000000000011324, 1.047197551196599630 ) ;
#30362=EDGE_CURVE ( 'NONE', #29483, #11737, #18161, .T. ) ;
#30395=DIRECTION ( 'NONE',  ( 0.000000000000000000, 0.000000000000000000, -1.000000000000000000 ) ) ;
#30402=DIRECTION ( 'NONE',  ( -2.157041537713702240E-32, 0.8709776783778059306, -0.4913225862583635584 ) ) ;
#30405=EDGE_LOOP ( 'NONE', ( #30678, #32872, #18283, #26866 ) ) ;
#30448=ORIENTED_EDGE ( 'NONE', *, *, #16779, .F. ) ;
#30451=CIRCLE ( 'NONE', #12071, 0.1000000000000000194 ) ;
#30461=AXIS2_PLACEMENT_3D ( 'NONE', #36653, #11757, #8458 ) ;
#30468=DIRECTION ( 'NONE',  ( 4.930380657631322689E-32, 0.7472307839325097456, 0.6645646360916346307 ) ) ;
#30506=ORIENTED_EDGE ( 'NONE', *, *, #26651, .T. ) ;
#30530=CARTESIAN_POINT ( 'NONE',  ( 0.000000000000000000, -0.4415087982045245996, -0.1343585914930099934 ) ) ;
#30541=AXIS2_PLACEMENT_3D ( 'NONE', #30242, #17512, #14609 ) ;
#30577=ADVANCED_FACE ( 'NONE', ( #31935 ), #37690, .F. ) ;
#30591=EDGE_CURVE ( 'NONE', #7881, #29289, #18981, .T. ) ;
#30609=CARTESIAN_POINT ( 'NONE',  ( 0.05999999999999990757, 0.8492681979939306069, -0.2138253033704803907 ) ) ;
#30624=CARTESIAN_POINT ( 'NONE',  ( 0.05999999999999990757, 0.000000000000000000, 0.000000000000000000 ) ) ;
#30632=DIRECTION ( 'NONE',  ( -1.000000000000000000, -7.857794173099924470E-32, -8.628166150854818811E-32 ) ) ;
#30659=DIRECTION ( 'NONE',  ( 0.000000000000000000, 0.000000000000000000, -1.000000000000000000 ) ) ;
#30678=ORIENTED_EDGE ( 'NONE', *, *, #26156, .F. ) ;
#30679=EDGE_CURVE ( 'NONE', #34841, #30067, #27282, .T. ) ;
#30734=DIRECTION ( 'NONE',  ( -1.000000000000000000, -7.857794173099924470E-32, -8.628166150854818811E-32 ) ) ;
#30782=CARTESIAN_POINT ( 'NONE',  ( 0.05999999999999990757, -0.4415087982045245996, -0.1343585914930097158 ) ) ;
#30795=ORIENTED_EDGE ( 'NONE', *, *, #24012, .F. ) ;
#30808=DIRECTION ( 'NONE',  ( 0.000000000000000000, 9.106159978880816258E-16, -1.000000000000000000 ) ) ;
#30834=DIRECTION ( 'NONE',  ( -0.8660254037844390407, 0.4259456949666814429, 0.2618592464270647624 ) ) ;
#30881=CARTESIAN_POINT ( 'NONE',  ( 0.03113248654051816583, 0.1428018198284763673, -0.2638325989215043466 ) ) ;
#30898=FACE_OUTER_BOUND ( 'NONE', #12253, .T. ) ;
#30905=ORIENTED_EDGE ( 'NONE', *, *, #20091, .T. ) ;
#30923=DIRECTION ( 'NONE',  ( 1.000000000000000000, 6.779273404243070203E-32, 4.314083075427408311E-32 ) ) ;
#30924=DIRECTION ( 'NONE',  ( 0.4999999999999988898, -0.8529728694000326961, -0.1497908010108632559 ) ) ;
#30935=FACE_OUTER_BOUND ( 'NONE', #31328, .T. ) ;
#30962=VERTEX_POINT ( 'NONE', #27996 ) ;
#31034=EDGE_CURVE ( 'NONE', #18976, #5233, #3708, .T. ) ;
#31048=EDGE_CURVE ( 'NONE', #3878, #28752, #17399, .T. ) ;
#31055=VERTEX_POINT ( 'NONE', #9864 ) ;
#31088=EDGE_CURVE ( 'NONE', #21667, #34841, #22436, .T. ) ;
#31112=DIRECTION ( 'NONE',  ( -0.4492559606623149349, 8.326672684688674053E-17, 0.8934030903289849057 ) ) ;
#31137=ORIENTED_EDGE ( 'NONE', *, *, #6126, .T. ) ;
#31141=CIRCLE ( 'NONE', #17362, 0.1550424246542357609 ) ;
#31201=DIRECTION ( 'NONE',  ( 1.000000000000000000, 6.779273404243070203E-32, 4.314083075427408311E-32 ) ) ;
#31252=VECTOR ( 'NONE', #34675, 39.37007874015748143 ) ;
#31267=CYLINDRICAL_SURFACE ( 'NONE', #15362, 0.1000000000000000194 ) ;
#31293=DIRECTION ( 'NONE',  ( 1.000000000000000000, 6.779273404243070203E-32, 4.314083075427408311E-32 ) ) ;
#31320=EDGE_CURVE ( 'NONE', #28752, #13663, #27925, .T. ) ;
#31328=EDGE_LOOP ( 'NONE', ( #34223, #10997, #27780, #17650 ) ) ;
#31435=VERTEX_POINT ( 'NONE', #21324 ) ;
#31460=LINE ( 'NONE', #3267, #2211 ) ;
#31501=ORIENTED_EDGE ( 'NONE', *, *, #35816, .F. ) ;
#31508=VERTEX_POINT ( 'NONE', #2788 ) ;
#31513=DIRECTION ( 'NONE',  ( 0.4999999999999990008, 0.5755298573121164774, -0.6471208413753150035 ) ) ;
#31555=ORIENTED_EDGE ( 'NONE', *, *, #28021, .T. ) ;
#31566=ORIENTED_EDGE ( 'NONE', *, *, #17975, .T. ) ;
#31596=CARTESIAN_POINT ( 'NONE',  ( 0.05999999999999990757, -0.3497707857934448938, -0.3763954645181781244 ) ) ;
#31631=EDGE_LOOP ( 'NONE', ( #4776, #37229, #23254, #6754 ) ) ;
#31709=AXIS2_PLACEMENT_3D ( 'NONE', #4711, #26759, #32294 ) ;
#31719=ORIENTED_EDGE ( 'NONE', *, *, #24012, .T. ) ;
#31750=CARTESIAN_POINT ( 'NONE',  ( 0.000000000000000000, 0.2954784694557334168, 0.05188905557145093855 ) ) ;
#31838=DIRECTION ( 'NONE',  ( -6.162975822039151309E-33, 0.000000000000000000, -1.000000000000000000 ) ) ;
#31852=CARTESIAN_POINT ( 'NONE',  ( 0.05999999999999990757, 7.654042494670956004E-18, -0.06250000000000000000 ) ) ;
#31873=LINE ( 'NONE', #16041, #5258 ) ;
#31880=ORIENTED_EDGE ( 'NONE', *, *, #9368, .F. ) ;
#31887=LINE ( 'NONE', #16056, #38490 ) ;
#31894=CARTESIAN_POINT ( 'NONE',  ( 0.03113248654051816583, 0.5878163732725504298, -0.1704268771689479434 ) ) ;
#31934=PLANE ( 'NONE',  #6553 ) ;
#31935=FACE_OUTER_BOUND ( 'NONE', #11999, .T. ) ;
#31967=AXIS2_PLACEMENT_3D ( 'NONE', #25228, #34073, #6296 ) ;
#31992=CARTESIAN_POINT ( 'NONE',  ( 0.05999999999999990757, -0.2940959072101921867, -0.05922497245433272495 ) ) ;
#31997=AXIS2_PLACEMENT_3D ( 'NONE', #33778, #15665, #34175 ) ;
#32034=ORIENTED_EDGE ( 'NONE', *, *, #35816, .T. ) ;
#32081=ORIENTED_EDGE ( 'NONE', *, *, #19687, .T. ) ;
#32098=EDGE_CURVE ( 'NONE', #13663, #14824, #35543, .T. ) ;
#32108=EDGE_CURVE ( 'NONE', #8681, #17043, #29562, .T. ) ;
#32119=ADVANCED_FACE ( 'NONE', ( #40069 ), #36598, .T. ) ;
#32130=DIRECTION ( 'NONE',  ( 0.000000000000000000, 0.000000000000000000, 1.000000000000000000 ) ) ;
#32186=CARTESIAN_POINT ( 'NONE',  ( 0.000000000000000000, 0.6304109427692223822, -0.1442409525262416947 ) ) ;
#32208=DIRECTION ( 'NONE',  ( 0.4999999999999985567, -0.7377595849475284684, -0.4535535192433764462 ) ) ;
#32230=DIRECTION ( 'NONE',  ( -9.860761315262646473E-32, -0.8518913899333638851, -0.5237184928541300799 ) ) ;
#32272=VERTEX_POINT ( 'NONE', #6333 ) ;
#32275=EDGE_CURVE ( 'NONE', #40017, #1162, #16011, .T. ) ;
#32282=AXIS2_PLACEMENT_3D ( 'NONE', #8860, #3290, #6776 ) ;
#32292=VECTOR ( 'NONE', #8670, 39.37007874015748143 ) ;
#32293=CARTESIAN_POINT ( 'NONE',  ( 0.03113248654051816583, -0.4578766358967566452, -0.4053162176620347945 ) ) ;
#32294=DIRECTION ( 'NONE',  ( 0.000000000000000000, 0.000000000000000000, 1.000000000000000000 ) ) ;
#32303=VERTEX_POINT ( 'NONE', #16222 ) ;
#32350=EDGE_LOOP ( 'NONE', ( #15768, #34615, #22969, #40044 ) ) ;
#32358=ORIENTED_EDGE ( 'NONE', *, *, #32634, .F. ) ;
#32393=CIRCLE ( 'NONE', #35694, 0.1050424246542346618 ) ;
#32412=CARTESIAN_POINT ( 'NONE',  ( -8.628166150854817443E-33, -3.491513147198971704E-33, 0.2000000000000000111 ) ) ;
#32429=CIRCLE ( 'NONE', #22626, 0.1499999999999989675 ) ;
#32460=CIRCLE ( 'NONE', #1635, 0.4614999999999880864 ) ;
#32523=ORIENTED_EDGE ( 'NONE', *, *, #23061, .F. ) ;
#32553=ADVANCED_FACE ( 'NONE', ( #12041 ), #31934, .F. ) ;
#32603=DIRECTION ( 'NONE',  ( 0.000000000000000000, 0.000000000000000000, -1.000000000000000000 ) ) ;
#32608=ORIENTED_EDGE ( 'NONE', *, *, #32098, .F. ) ;
#32634=EDGE_CURVE ( 'NONE', #23647, #34438, #7211, .T. ) ;
#32686=EDGE_LOOP ( 'NONE', ( #23351, #9907, #13835, #9954 ) ) ;
#32834=DIRECTION ( 'NONE',  ( -1.000000000000000000, -6.779273404243070203E-32, -4.314083075427408311E-32 ) ) ;
#32847=EDGE_CURVE ( 'NONE', #14101, #16124, #14421, .T. ) ;
#32864=DIRECTION ( 'NONE',  ( -1.000000000000000000, -7.857794173099924470E-32, -8.628166150854818811E-32 ) ) ;
#32872=ORIENTED_EDGE ( 'NONE', *, *, #11507, .T. ) ;
#32928=EDGE_CURVE ( 'NONE', #23647, #8779, #34419, .T. ) ;
#32930=CARTESIAN_POINT ( 'NONE',  ( 0.05999999999999990757, 0.2165002077672316116, -0.1331859471648322857 ) ) ;
#33030=ORIENTED_EDGE ( 'NONE', *, *, #34164, .F. ) ;
#33054=VECTOR ( 'NONE', #14897, 39.37007874015748854 ) ;
#33104=DIRECTION ( 'NONE',  ( 0.000000000000000000, 0.000000000000000000, -1.000000000000000000 ) ) ;
#33125=AXIS2_PLACEMENT_3D ( 'NONE', #5734, #30214, #36605 ) ;
#33143=ORIENTED_EDGE ( 'NONE', *, *, #6498, .T. ) ;
#33146=AXIS2_PLACEMENT_3D ( 'NONE', #28806, #19741, #28997 ) ;
#33172=EDGE_CURVE ( 'NONE', #29483, #892, #37028, .T. ) ;
#33196=ORIENTED_EDGE ( 'NONE', *, *, #36675, .T. ) ;
#33229=VECTOR ( 'NONE', #23160, 39.37007874015748143 ) ;
#33248=CARTESIAN_POINT ( 'NONE',  ( 0.000000000000000000, 0.000000000000000000, 0.000000000000000000 ) ) ;
#33276=ORIENTED_EDGE ( 'NONE', *, *, #30362, .T. ) ;
#33279=CARTESIAN_POINT ( 'NONE',  ( 0.05999999999999990757, 0.000000000000000000, 0.000000000000000000 ) ) ;
#33292=DIRECTION ( 'NONE',  ( 1.000000000000000000, 6.779273404243070203E-32, 4.314083075427408311E-32 ) ) ;
#33308=DIRECTION ( 'NONE',  ( 0.000000000000000000, 1.776356839400250465E-15, -1.000000000000000000 ) ) ;
#33330=ORIENTED_EDGE ( 'NONE', *, *, #23245, .T. ) ;
#33397=DIRECTION ( 'NONE',  ( -1.000000000000000000, -7.857794173099924470E-32, -8.628166150854818811E-32 ) ) ;
#33404=ADVANCED_FACE ( 'NONE', ( #24080 ), #39026, .T. ) ;
#33410=FACE_OUTER_BOUND ( 'NONE', #13568, .T. ) ;
#33445=EDGE_CURVE ( 'NONE', #20959, #14789, #37736, .T. ) ;
#33453=DIRECTION ( 'NONE',  ( 1.000000000000000000, 6.779273404243070203E-32, 4.314083075427408311E-32 ) ) ;
#33499=PRODUCT_CONTEXT ( 'NONE', #12985, 'mechanical' ) ;
#33504=FACE_OUTER_BOUND ( 'NONE', #39560, .T. ) ;
#33505=FACE_OUTER_BOUND ( 'NONE', #29230, .T. ) ;
#33536=ADVANCED_FACE ( 'NONE', ( #34318 ), #6131, .F. ) ;
#33580=AXIS2_PLACEMENT_3D ( 'NONE', #18561, #5995, #6207 ) ;
#33593=ORIENTED_EDGE ( 'NONE', *, *, #6498, .F. ) ;
#33630=ORIENTED_EDGE ( 'NONE', *, *, #22513, .F. ) ;
#33631=VERTEX_POINT ( 'NONE', #2360 ) ;
#33633=ORIENTED_EDGE ( 'NONE', *, *, #33445, .T. ) ;
#33641=ADVANCED_FACE ( 'NONE', ( #34423 ), #6239, .F. ) ;
#33671=EDGE_CURVE ( 'NONE', #38278, #34438, #5516, .T. ) ;
#33709=CIRCLE ( 'NONE', #2188, 0.1000000000000000194 ) ;
#33778=CARTESIAN_POINT ( 'NONE',  ( 0.000000000000000000, 0.000000000000000000, 0.000000000000000000 ) ) ;
#33835=CARTESIAN_POINT ( 'NONE',  ( 0.03113248654051816583, -3.491513147198971704E-33, 0.2000000000000000111 ) ) ;
#33951=ORIENTED_EDGE ( 'NONE', *, *, #33671, .T. ) ;
#34013=CARTESIAN_POINT ( 'NONE',  ( 0.03113248654051816583, 0.1969856463038233696, 0.03459270371430114843 ) ) ;
#34073=DIRECTION ( 'NONE',  ( -1.000000000000000000, -7.857794173099924470E-32, -8.628166150854818811E-32 ) ) ;
#34112=FACE_OUTER_BOUND ( 'NONE', #35004, .T. ) ;
#34136=CARTESIAN_POINT ( 'NONE',  ( 0.05999999999999990757, -0.2461558908287989345, -0.2173297548048775396 ) ) ;
#34164=EDGE_CURVE ( 'NONE', #553, #34841, #33709, .T. ) ;
#34175=DIRECTION ( 'NONE',  ( -6.162975822039154730E-33, 0.000000000000000000, -1.000000000000000000 ) ) ;
#34185=VERTEX_POINT ( 'NONE', #32293 ) ;
#34209=ADVANCED_FACE ( 'NONE', ( #12781 ), #16470, .T. ) ;
#34223=ORIENTED_EDGE ( 'NONE', *, *, #9989, .F. ) ;
#34226=FACE_OUTER_BOUND ( 'NONE', #12429, .T. ) ;
#34240=CARTESIAN_POINT ( 'NONE',  ( 0.05999999999999990757, 0.000000000000000000, 0.000000000000000000 ) ) ;
#34299=ORIENTED_EDGE ( 'NONE', *, *, #32108, .F. ) ;
#34306=ORIENTED_EDGE ( 'NONE', *, *, #29769, .T. ) ;
#34311=CARTESIAN_POINT ( 'NONE',  ( 0.03113248654051816583, -0.03575622569115821658, -0.2978615321325044363 ) ) ;
#34318=FACE_OUTER_BOUND ( 'NONE', #37275, .T. ) ;
#34419=CIRCLE ( 'NONE', #30461, 0.1000000000000000194 ) ;
#34423=FACE_OUTER_BOUND ( 'NONE', #9953, .T. ) ;
#34432=AXIS2_PLACEMENT_3D ( 'NONE', #23595, #35496, #4239 ) ;
#34438=VERTEX_POINT ( 'NONE', #26712 ) ;
#34445=AXIS2_PLACEMENT_3D ( 'NONE', #12015, #28066, #24574 ) ;
#34475=DIRECTION ( 'NONE',  ( -6.162975822039154730E-33, 0.000000000000000000, -1.000000000000000000 ) ) ;
#34476=FACE_OUTER_BOUND ( 'NONE', #25145, .T. ) ;
#34477=VECTOR ( 'NONE', #34868, 39.37007874015748143 ) ;
#34502=CARTESIAN_POINT ( 'NONE',  ( 0.05999999999999990757, -0.2940959072101921867, -0.05922497245433272495 ) ) ;
#34615=ORIENTED_EDGE ( 'NONE', *, *, #7887, .T. ) ;
#34648=ORIENTED_EDGE ( 'NONE', *, *, #10168, .F. ) ;
#34649=VERTEX_POINT ( 'NONE', #18648 ) ;
#34669=DIRECTION ( 'NONE',  ( 0.000000000000000000, 0.000000000000000000, -1.000000000000000000 ) ) ;
#34675=DIRECTION ( 'NONE',  ( 0.4999999999999984457, 0.4254978411528151372, 0.7542887956043727860 ) ) ;
#34743=ORIENTED_EDGE ( 'NONE', *, *, #35578, .T. ) ;
#34780=EDGE_CURVE ( 'NONE', #8681, #31055, #13869, .T. ) ;
#34783=EDGE_CURVE ( 'NONE', #22334, #27427, #17384, .T. ) ;
#34841=VERTEX_POINT ( 'NONE', #36290 ) ;
#34843=EDGE_CURVE ( 'NONE', #11737, #34649, #25862, .T. ) ;
#34868=DIRECTION ( 'NONE',  ( -1.000000000000000000, -7.857794173099924470E-32, -8.628166150854818811E-32 ) ) ;
#34915=AXIS2_PLACEMENT_3D ( 'NONE', #36547, #14329, #26890 ) ;
#34952=CARTESIAN_POINT ( 'NONE',  ( 0.05999999999999990757, 0.000000000000000000, 0.000000000000000000 ) ) ;
#34964=DIRECTION ( 'NONE',  ( 0.000000000000000000, 0.000000000000000000, -1.000000000000000000 ) ) ;
#34977=DIRECTION ( 'NONE',  ( 1.000000000000000000, 6.779273404243070203E-32, 4.314083075427408311E-32 ) ) ;
#35004=EDGE_LOOP ( 'NONE', ( #39122, #10528, #37038, #24157 ) ) ;
#35038=ORIENTED_EDGE ( 'NONE', *, *, #5688, .T. ) ;
#35130=ADVANCED_FACE ( 'NONE', ( #33504 ), #31267, .T. ) ;
#35219=CARTESIAN_POINT ( 'NONE',  ( 0.000000000000000000, 0.7171888913565960255, -0.2950238883388468514 ) ) ;
#35248=CIRCLE ( 'NONE', #8312, 0.4614999999999880864 ) ;
#35390=CARTESIAN_POINT ( 'NONE',  ( 0.03113248654051816583, 0.5878163732725504298, -0.1704268771689479434 ) ) ;
#35412=VERTEX_POINT ( 'NONE', #6086 ) ;
#35496=DIRECTION ( 'NONE',  ( -1.000000000000000000, -7.857794173099924470E-32, -8.628166150854818811E-32 ) ) ;
#35543=CIRCLE ( 'NONE', #15200, 0.1000000000000000194 ) ;
#35558=VERTEX_POINT ( 'NONE', #10600 ) ;
#35578=EDGE_CURVE ( 'NONE', #23080, #39766, #31141, .T. ) ;
#35587=CARTESIAN_POINT ( 'NONE',  ( 0.03113248654051816583, -0.03575622569115821658, -0.1978615321325044307 ) ) ;
#35645=AXIS2_PLACEMENT_3D ( 'NONE', #16239, #19525, #7336 ) ;
#35694=AXIS2_PLACEMENT_3D ( 'NONE', #22318, #10162, #38331 ) ;
#35707=ORIENTED_EDGE ( 'NONE', *, *, #30679, .F. ) ;
#35779=ORIENTED_EDGE ( 'NONE', *, *, #29072, .F. ) ;
#35816=EDGE_CURVE ( 'NONE', #24060, #20188, #39024, .T. ) ;
#35849=VECTOR ( 'NONE', #13323, 39.37007874015748143 ) ;
#35888=ORIENTED_EDGE ( 'NONE', *, *, #8470, .F. ) ;
#35893=AXIS2_PLACEMENT_3D ( 'NONE', #12021, #21289, #24578 ) ;
#35899=DIRECTION ( 'NONE',  ( 0.000000000000000000, 0.000000000000000000, -1.000000000000000000 ) ) ;
#35924=FACE_OUTER_BOUND ( 'NONE', #17562, .T. ) ;
#35935=ADVANCED_FACE ( 'NONE', ( #28711 ), #27876, .F. ) ;
#35942=DIRECTION ( 'NONE',  ( 0.000000000000000000, 0.000000000000000000, -1.000000000000000000 ) ) ;
#35955=FACE_OUTER_BOUND ( 'NONE', #7967, .T. ) ;
#35970=DIRECTION ( 'NONE',  ( 1.000000000000000000, 7.857794173099924470E-32, 8.628166150854818811E-32 ) ) ;
#36038=EDGE_CURVE ( 'NONE', #28752, #29747, #40440, .T. ) ;
#36095=CARTESIAN_POINT ( 'NONE',  ( 0.05999999999999990757, 0.000000000000000000, 0.4614999999999880864 ) ) ;
#36107=CYLINDRICAL_SURFACE ( 'NONE', #9880, 0.2000000000000000111 ) ;
#36131=EDGE_CURVE ( 'NONE', #18976, #20310, #343, .T. ) ;
#36176=ORIENTED_EDGE ( 'NONE', *, *, #3045, .T. ) ;
#36199=AXIS2_PLACEMENT_3D ( 'NONE', #29557, #32834, #26700 ) ;
#36221=ORIENTED_EDGE ( 'NONE', *, *, #38921, .F. ) ;
#36229=DIRECTION ( 'NONE',  ( -1.000000000000000000, -7.857794173099924470E-32, -8.628166150854818811E-32 ) ) ;
#36289=DIRECTION ( 'NONE',  ( -0.4999999999999980016, -0.1032193326399760414, -0.8598521787896800106 ) ) ;
#36290=CARTESIAN_POINT ( 'NONE',  ( -4.314083075427408721E-33, 0.1428018198284763673, -0.1638325989215043410 ) ) ;
#36314=ORIENTED_EDGE ( 'NONE', *, *, #21233, .F. ) ;
#36317=ORIENTED_EDGE ( 'NONE', *, *, #23735, .F. ) ;
#36329=APPLICATION_CONTEXT ( 'configuration controlled 3d designs of mechanical parts and assemblies' ) ;
#36339=CARTESIAN_POINT ( 'NONE',  ( 0.03113248654051816583, -0.3458405862425447119, -0.1052451372150005060 ) ) ;
#36365=CARTESIAN_POINT ( 'NONE',  ( 0.05999999999999990757, 0.5878163732725504298, -0.1704268771689479434 ) ) ;
#36379=DIRECTION ( 'NONE',  ( 1.000000000000000000, 6.779273404243070203E-32, 4.314083075427407763E-32 ) ) ;
#36385=VECTOR ( 'NONE', #39328, 39.37007874015748143 ) ;
#36547=CARTESIAN_POINT ( 'NONE',  ( 0.05999999999999990757, 0.000000000000000000, 0.000000000000000000 ) ) ;
#36584=AXIS2_PLACEMENT_3D ( 'NONE', #22308, #27865, #18600 ) ;
#36588=CARTESIAN_POINT ( 'NONE',  ( 0.05999999999999990757, 0.7171888913565960255, -0.2325238883388469069 ) ) ;
#36592=CARTESIAN_POINT ( 'NONE',  ( 0.000000000000000000, -0.1960639381401260983, -0.03948331496955503200 ) ) ;
#36598=CYLINDRICAL_SURFACE ( 'NONE', #7961, 0.1550424246542357609 ) ;
#36600=CARTESIAN_POINT ( 'NONE',  ( 0.03113248654051816583, -0.3165425539888620521, -0.4137570037148034507 ) ) ;
#36605=DIRECTION ( 'NONE',  ( 0.000000000000000000, 0.000000000000000000, 1.000000000000000000 ) ) ;
#36606=FACE_OUTER_BOUND ( 'NONE', #7682, .T. ) ;
#36653=CARTESIAN_POINT ( 'NONE',  ( 0.000000000000000000, -0.3829990175980249600, -0.3390339253215535198 ) ) ;
#36675=EDGE_CURVE ( 'NONE', #27427, #3365, #2948, .T. ) ;
#36720=FACE_OUTER_BOUND ( 'NONE', #8389, .T. ) ;
#36740=DIRECTION ( 'NONE',  ( -1.000000000000000000, -7.857794173099924470E-32, -8.628166150854818811E-32 ) ) ;
#36744=PLANE ( 'NONE',  #27318 ) ;
#36783=AXIS2_PLACEMENT_3D ( 'NONE', #37317, #6253, #12843 ) ;
#36855=CARTESIAN_POINT ( 'NONE',  ( 0.05999999999999990757, -0.3497707857934448938, -0.3763954645181781244 ) ) ;
#36857=DIRECTION ( 'NONE',  ( 1.000000000000000000, 6.779273404243070203E-32, 4.314083075427408311E-32 ) ) ;
#36866=ORIENTED_EDGE ( 'NONE', *, *, #20623, .T. ) ;
#36925=PLANE ( 'NONE',  #6847 ) ;
#36948=LINE ( 'NONE', #30782, #34477 ) ;
#36949=DIRECTION ( 'NONE',  ( -4.930380657631322689E-32, -0.7472307839325097456, -0.6645646360916346307 ) ) ;
#36956=LINE ( 'NONE', #31596, #23458 ) ;
#36977=ORIENTED_EDGE ( 'NONE', *, *, #37400, .T. ) ;
#36991=ORIENTED_EDGE ( 'NONE', *, *, #12947, .T. ) ;
#36995=DIRECTION ( 'NONE',  ( 0.000000000000000000, 0.000000000000000000, 1.000000000000000000 ) ) ;
#37028=CIRCLE ( 'NONE', #21309, 0.04999999999999994726 ) ;
#37038=ORIENTED_EDGE ( 'NONE', *, *, #8223, .F. ) ;
#37064=ADVANCED_FACE ( 'NONE', ( #19102 ), #19902, .T. ) ;
#37090=AXIS2_PLACEMENT_3D ( 'NONE', #7268, #1348, #17159 ) ;
#37093=CARTESIAN_POINT ( 'NONE',  ( 0.03113248654051816583, -3.491513147198971704E-33, 0.4614999999999880864 ) ) ;
#37112=EDGE_CURVE ( 'NONE', #26563, #38515, #14779, .T. ) ;
#37137=CARTESIAN_POINT ( 'NONE',  ( 0.05999999999999990757, 0.8492681979939306069, -0.2138253033704805295 ) ) ;
#37154=DIRECTION ( 'NONE',  ( -1.000000000000000000, -6.779273404243070203E-32, -4.314083075427408311E-32 ) ) ;
#37225=CARTESIAN_POINT ( 'NONE',  ( 0.05999999999999990757, -0.3829990175980249600, -0.3390339253215535198 ) ) ;
#37229=ORIENTED_EDGE ( 'NONE', *, *, #25802, .F. ) ;
#37239=VERTEX_POINT ( 'NONE', #14134 ) ;
#37271=DIRECTION ( 'NONE',  ( 0.4999999999999991118, 0.5755298573121168104, -0.6471208413753148925 ) ) ;
#37275=EDGE_LOOP ( 'NONE', ( #21375, #19988, #29947, #1241, #18387 ) ) ;
#37294=ORIENTED_EDGE ( 'NONE', *, *, #26093, .T. ) ;
#37298=EDGE_CURVE ( 'NONE', #33631, #31055, #37765, .T. ) ;
#37317=CARTESIAN_POINT ( 'NONE',  ( 0.03113248654051816583, 0.000000000000000000, 0.000000000000000000 ) ) ;
#37326=CARTESIAN_POINT ( 'NONE',  ( 0.05999999999999990757, 9.785038312124675210E-34, 0.1499999999999990785 ) ) ;
#37349=FACE_OUTER_BOUND ( 'NONE', #20588, .T. ) ;
#37400=EDGE_CURVE ( 'NONE', #26563, #3365, #36948, .T. ) ;
#37405=EDGE_CURVE ( 'NONE', #39909, #38544, #19405, .T. ) ;
#37468=CARTESIAN_POINT ( 'NONE',  ( 0.03113248654051816583, 0.8492681979939306069, -0.2138253033704803907 ) ) ;
#37477=AXIS2_PLACEMENT_3D ( 'NONE', #12432, #18832, #24984 ) ;
#37509=ORIENTED_EDGE ( 'NONE', *, *, #5436, .T. ) ;
#37541=CIRCLE ( 'NONE', #19815, 0.1500000000000011324 ) ;
#37583=ADVANCED_FACE ( 'NONE', ( #21229 ), #8657, .F. ) ;
#37621=ADVANCED_FACE ( 'NONE', ( #12778 ), #22059, .F. ) ;
#37660=DIRECTION ( 'NONE',  ( 0.000000000000000000, 0.000000000000000000, -1.000000000000000000 ) ) ;
#37665=DIRECTION ( 'NONE',  ( -1.000000000000000000, -7.857794173099924470E-32, -8.628166150854818811E-32 ) ) ;
#37676=AXIS2_PLACEMENT_3D ( 'NONE', #14481, #8108, #17592 ) ;
#37690=CYLINDRICAL_SURFACE ( 'NONE', #27899, 0.1000000000000000194 ) ;
#37697=CIRCLE ( 'NONE', #21951, 0.1000000000000008521 ) ;
#37726=( GEOMETRIC_REPRESENTATION_CONTEXT ( 3 ) GLOBAL_UNCERTAINTY_ASSIGNED_CONTEXT ( ( #3007 ) ) GLOBAL_UNIT_ASSIGNED_CONTEXT ( ( #7004, #28015, #28411 ) ) REPRESENTATION_CONTEXT ( 'NONE', 'WORKASPACE' ) );
#37734=VERTEX_POINT ( 'NONE', #18536 ) ;
#37736=CIRCLE ( 'NONE', #15400, 0.6114999999999938263 ) ;
#37761=AXIS2_PLACEMENT_3D ( 'NONE', #15724, #22327, #9560 ) ;
#37764=DIRECTION ( 'NONE',  ( 0.000000000000000000, 0.000000000000000000, -1.000000000000000000 ) ) ;
#37765=CIRCLE ( 'NONE', #23987, 0.06250000000000000000 ) ;
#37798=ORIENTED_EDGE ( 'NONE', *, *, #39859, .T. ) ;
#37820=CARTESIAN_POINT ( 'NONE',  ( 0.03113248654051816583, 0.09520121321898405986, -0.1758883992810029440 ) ) ;
#37842=ORIENTED_EDGE ( 'NONE', *, *, #31088, .T. ) ;
#37849=ORIENTED_EDGE ( 'NONE', *, *, #8472, .T. ) ;
#37863=VERTEX_POINT ( 'NONE', #13166 ) ;
#37970=CARTESIAN_POINT ( 'NONE',  ( 0.05999999999999990757, 0.000000000000000000, 0.000000000000000000 ) ) ;
#38023=CARTESIAN_POINT ( 'NONE',  ( -4.314083075427408721E-33, -0.03575622569115821658, -0.1978615321325044307 ) ) ;
#38056=FACE_OUTER_BOUND ( 'NONE', #8200, .T. ) ;
#38090=ORIENTED_EDGE ( 'NONE', *, *, #28811, .T. ) ;
#38133=VECTOR ( 'NONE', #39301, 39.37007874015748854 ) ;
#38141=ORIENTED_EDGE ( 'NONE', *, *, #17292, .T. ) ;
#38147=ADVANCED_FACE ( 'NONE', ( #21789 ), #15616, .F. ) ;
#38182=CARTESIAN_POINT ( 'NONE',  ( 0.000000000000000000, -0.4578766358967566452, -0.4053162176620347945 ) ) ;
#38205=DIRECTION ( 'NONE',  ( -1.000000000000000000, -7.857794173099924470E-32, -8.628166150854818811E-32 ) ) ;
#38276=VERTEX_POINT ( 'NONE', #4461 ) ;
#38278=VERTEX_POINT ( 'NONE', #38023 ) ;
#38325=CARTESIAN_POINT ( 'NONE',  ( 0.05999999999999990757, -0.3458405862425447119, -0.2552451372150014719 ) ) ;
#38331=DIRECTION ( 'NONE',  ( 0.000000000000000000, 0.000000000000000000, -1.000000000000000000 ) ) ;
#38337=AXIS2_PLACEMENT_3D ( 'NONE', #34502, #14974, #30808 ) ;
#38376=DIRECTION ( 'NONE',  ( 0.8660254037844395958, -0.2456612931291811963, -0.4354888391889014110 ) ) ;
#38384=LINE ( 'NONE', #16805, #5491 ) ;
#38446=DIRECTION ( 'NONE',  ( 0.4999999999999988898, -0.8285110189370871181, -0.2521299099667287935 ) ) ;
#38490=VECTOR ( 'NONE', #3892, 39.37007874015748143 ) ;
#38500=DIRECTION ( 'NONE',  ( 1.000000000000000000, 6.779273404243070203E-32, 4.314083075427408311E-32 ) ) ;
#38515=VERTEX_POINT ( 'NONE', #26899 ) ;
#38544=VERTEX_POINT ( 'NONE', #8161 ) ;
#38569=FACE_OUTER_BOUND ( 'NONE', #1002, .T. ) ;
#38607=EDGE_LOOP ( 'NONE', ( #32358, #25366, #29438, #16093, #4527, #16753, #31880, #12491, #12315, #20870, #402, #33951 ) ) ;
#38616=ORIENTED_EDGE ( 'NONE', *, *, #8472, .F. ) ;
#38627=DIRECTION ( 'NONE',  ( -1.000000000000000000, -6.779273404243070203E-32, -4.314083075427408311E-32 ) ) ;
#38641=DIRECTION ( 'NONE',  ( 1.000000000000000000, 6.779273404243070203E-32, 4.314083075427407763E-32 ) ) ;
#38656=CARTESIAN_POINT ( 'NONE',  ( 0.03113248654051843992, 0.6304109427692223822, -0.1442409525262416947 ) ) ;
#38695=ORIENTED_EDGE ( 'NONE', *, *, #18426, .F. ) ;
#38702=DIRECTION ( 'NONE',  ( -1.232595164407830672E-32, -0.6645646360916346307, 0.7472307839325098566 ) ) ;
#38735=ORIENTED_EDGE ( 'NONE', *, *, #12947, .F. ) ;
#38804=VECTOR ( 'NONE', #25356, 39.37007874015748854 ) ;
#38831=EDGE_CURVE ( 'NONE', #32272, #32303, #24743, .T. ) ;
#38844=ORIENTED_EDGE ( 'NONE', *, *, #10262, .F. ) ;
#38860=EDGE_CURVE ( 'NONE', #37863, #5937, #26068, .T. ) ;
#38891=ORIENTED_EDGE ( 'NONE', *, *, #21073, .T. ) ;
#38919=( LENGTH_UNIT ( ) NAMED_UNIT ( * ) SI_UNIT ( $, .METRE. ) );
#38921=EDGE_CURVE ( 'NONE', #1162, #22334, #35248, .T. ) ;
#38922=CARTESIAN_POINT ( 'NONE',  ( 0.05999999999999990757, -0.3458405862425447119, -0.1052451372150005060 ) ) ;
#38972=ADVANCED_FACE ( 'NONE', ( #24967 ), #27463, .F. ) ;
#38986=ORIENTED_EDGE ( 'NONE', *, *, #34783, .F. ) ;
#39000=FACE_BOUND ( 'NONE', #7164, .T. ) ;
#39018=VECTOR ( 'NONE', #5947, 39.37007874015748143 ) ;
#39024=CIRCLE ( 'NONE', #19342, 0.1500000000000011324 ) ;
#39026=CONICAL_SURFACE ( 'NONE', #33125, 0.1050424246542346202, 1.047197551196599852 ) ;
#39078=VECTOR ( 'NONE', #6375, 39.37007874015748143 ) ;
#39080=AXIS2_PLACEMENT_3D ( 'NONE', #12005, #30923, #17970 ) ;
#39093=AXIS2_PLACEMENT_3D ( 'NONE', #624, #32230, #4048 ) ;
#39122=ORIENTED_EDGE ( 'NONE', *, *, #32847, .F. ) ;
#39134=DIRECTION ( 'NONE',  ( 1.000000000000000000, 7.857794173099924470E-32, 8.628166150854818811E-32 ) ) ;
#39196=CONICAL_SURFACE ( 'NONE', #31967, 0.04999999999999888561, 1.047197551196599630 ) ;
#39211=DIRECTION ( 'NONE',  ( 0.000000000000000000, 0.000000000000000000, 1.000000000000000000 ) ) ;
#39216=FACE_BOUND ( 'NONE', #14011, .T. ) ;
#39229=VECTOR ( 'NONE', #24581, 39.37007874015748143 ) ;
#39297=ORIENTED_EDGE ( 'NONE', *, *, #7725, .T. ) ;
#39300=ORIENTED_EDGE ( 'NONE', *, *, #5436, .F. ) ;
#39301=DIRECTION ( 'NONE',  ( -0.4999999999999986677, 0.4122333455936965096, -0.7616191100416460635 ) ) ;
#39307=EDGE_CURVE ( 'NONE', #13712, #22389, #3714, .T. ) ;
#39328=DIRECTION ( 'NONE',  ( -1.000000000000000000, -6.779273404243070203E-32, -4.314083075427407763E-32 ) ) ;
#39388=EDGE_CURVE ( 'NONE', #3365, #35412, #7013, .T. ) ;
#39420=CARTESIAN_POINT ( 'NONE',  ( 0.05999999999999990757, 0.09520121321898405986, -0.1758883992810029440 ) ) ;
#39424=CIRCLE ( 'NONE', #12498, 0.2000000000000000111 ) ;
#39501=DIRECTION ( 'NONE',  ( 1.000000000000000000, 6.779273404243070203E-32, 4.314083075427408311E-32 ) ) ;
#39560=EDGE_LOOP ( 'NONE', ( #26583, #12270, #11745, #24096 ) ) ;
#39565=ADVANCED_FACE ( 'NONE', ( #13109 ), #25670, .T. ) ;
#39568=AXIS2_PLACEMENT_3D ( 'NONE', #29938, #11201, #20681 ) ;
#39616=ORIENTED_EDGE ( 'NONE', *, *, #19648, .T. ) ;
#39620=ORIENTED_EDGE ( 'NONE', *, *, #27361, .T. ) ;
#39733=DIRECTION ( 'NONE',  ( -6.162975822039154046E-33, 0.000000000000000000, -1.000000000000000000 ) ) ;
#39758=ORIENTED_EDGE ( 'NONE', *, *, #24263, .F. ) ;
#39762=ORIENTED_EDGE ( 'NONE', *, *, #16701, .T. ) ;
#39766=VERTEX_POINT ( 'NONE', #1996 ) ;
#39792=CARTESIAN_POINT ( 'NONE',  ( 0.03113248654051816583, 0.000000000000000000, 0.000000000000000000 ) ) ;
#39804=AXIS2_PLACEMENT_3D ( 'NONE', #27887, #12251, #27481 ) ;
#39823=DIRECTION ( 'NONE',  ( 1.000000000000000000, 6.779273404243070203E-32, 4.314083075427408311E-32 ) ) ;
#39835=DIRECTION ( 'NONE',  ( 0.000000000000000000, 0.000000000000000000, 1.000000000000000000 ) ) ;
#39859=EDGE_CURVE ( 'NONE', #8779, #34185, #4152, .T. ) ;
#39866=DIRECTION ( 'NONE',  ( 1.000000000000000000, 6.779273404243070203E-32, 4.314083075427408311E-32 ) ) ;
#39909=VERTEX_POINT ( 'NONE', #29266 ) ;
#39960=ORIENTED_EDGE ( 'NONE', *, *, #35578, .F. ) ;
#40017=VERTEX_POINT ( 'NONE', #218 ) ;
#40044=ORIENTED_EDGE ( 'NONE', *, *, #32634, .T. ) ;
#40053=EDGE_LOOP ( 'NONE', ( #26419, #7748 ) ) ;
#40069=FACE_OUTER_BOUND ( 'NONE', #513, .T. ) ;
#40131=DIRECTION ( 'NONE',  ( -1.000000000000000000, -7.857794173099924470E-32, -8.628166150854818811E-32 ) ) ;
#40144=EDGE_LOOP ( 'NONE', ( #25514, #4406, #34648, #20401 ) ) ;
#40161=CARTESIAN_POINT ( 'NONE',  ( 0.000000000000000000, 0.1369749717427355129, -0.1457321416712075435 ) ) ;
#40279=DIRECTION ( 'NONE',  ( 0.000000000000000000, 0.000000000000000000, 1.000000000000000000 ) ) ;
#40316=ORIENTED_EDGE ( 'NONE', *, *, #28021, .F. ) ;
#40317=FACE_OUTER_BOUND ( 'NONE', #21438, .T. ) ;
#40376=DIRECTION ( 'NONE',  ( -1.540743955509787314E-32, 0.8709776783778059306, -0.4913225862583634473 ) ) ;
#40421=DIRECTION ( 'NONE',  ( 4.930380657631323784E-32, 0.7472307839325098566, 0.6645646360916346307 ) ) ;
#40432=EDGE_CURVE ( 'NONE', #34649, #24445, #22551, .T. ) ;
#40440=LINE ( 'NONE', #24821, #12112 ) ;
#40449=CARTESIAN_POINT ( 'NONE',  ( 0.000000000000000000, 0.000000000000000000, 0.000000000000000000 ) ) ;
#40493=ORIENTED_EDGE ( 'NONE', *, *, #16701, .F. ) ;
#40521=DIRECTION ( 'NONE',  ( -4.930380657631323784E-32, -0.7472307839325098566, -0.6645646360916346307 ) ) ;
#40576=ORIENTED_EDGE ( 'NONE', *, *, #9989, .T. ) ;
#40590=LINE ( 'NONE', #12219, #22578 ) ;
#40702=COLOUR_RGB('Off White',0.89,0.88,0.83);
#40703=FILL_AREA_STYLE_COLOUR('',#40702);
#40704=FILL_AREA_STYLE('',(#40703));
#40705=SURFACE_STYLE_FILL_AREA(#40704);
#40706=SURFACE_SIDE_STYLE('',(#40705));
#40707=SURFACE_STYLE_USAGE(.BOTH.,#40706);
#40708=PRESENTATION_STYLE_ASSIGNMENT((#40707));
#40713=STYLED_ITEM('',(#40708),#18866);
#40721=MECHANICAL_DESIGN_GEOMETRIC_PRESENTATION_REPRESENTATION('',(#40713),#11399);
ENDSEC;
END-ISO-10303-21;
